ISO-10303-21;
HEADER;
FILE_DESCRIPTION (('STEP AP214'),
    '1' );
FILE_NAME ('Spring.step',
    '2026-10-21T18:31:44',
    ( '' ),
    ( '' ),
    'SwSTEP 2.0',
    'SolidWorks 2025',
    '' );
FILE_SCHEMA (( 'AUTOMOTIVE_DESIGN' ));
ENDSEC;

DATA;
#21=CARTESIAN_POINT ( 'NONE',  ( -13.16986379959834252, -72.84374999999981526, -13.16986379960055054 ) ) ;
#32=CARTESIAN_POINT ( 'NONE',  ( 15.00000000000000000, -99.89999999999999147, 0.000000000000000000 ) ) ;
#33=CARTESIAN_POINT ( 'NONE',  ( -11.37500000000000178, -84.32499999999977547, -9.545674412382054647E-13 ) ) ;
#45=CARTESIAN_POINT ( 'NONE',  ( 8.043339635996298753, -88.41874999999980389, 8.043339635997652337 ) ) ;
#52=CARTESIAN_POINT ( 'NONE',  ( 7.714727599200456254, -45.82187499999987779, -18.62499999999935341 ) ) ;
#55=CARTESIAN_POINT ( 'NONE',  ( -7.714727599197334307, 2.046875000000014211, -18.62500000000064659 ) ) ;
#77=CARTESIAN_POINT ( 'NONE',  ( 8.043339635996298753, -105.0687499999997527, 8.043339635997652337 ) ) ;
#87=CARTESIAN_POINT ( 'NONE',  ( 8.043339635997654113, -18.73124999999995666, -8.043339635996304082 ) ) ;
#88=CARTESIAN_POINT ( 'NONE',  ( -13.16986379960055231, -43.70624999999989768, 13.16986379959834252 ) ) ;
#93=CARTESIAN_POINT ( 'NONE',  ( 15.91271015948297141, 2.066541229842319115E-14, -9.178967570126440378 ) ) ;
#123=CARTESIAN_POINT ( 'NONE',  ( 4.163872747629839388, -100.0000000000000426, 15.14667126703698585 ) ) ;
#125=CARTESIAN_POINT ( 'NONE',  ( -11.37500000000000000, -41.62499999999990052, -9.545674412382054647E-13 ) ) ;
#136=CARTESIAN_POINT ( 'NONE',  ( 13.16986379960055409, -42.63124999999990905, -13.16986379959834430 ) ) ;
#144=CARTESIAN_POINT ( 'NONE',  ( -13.16986379959834252, -65.59374999999981526, -13.16986379960055409 ) ) ;
#146=CARTESIAN_POINT ( 'NONE',  ( 18.62500000000000000, -75.99999999999980105, 1.560692158462880521E-12 ) ) ;
#171=CARTESIAN_POINT ( 'NONE',  ( -11.37500000000039613, -83.21562499999981810, 4.711679271993000739 ) ) ;
#184=CARTESIAN_POINT ( 'NONE',  ( 3.512344863372272030, -7.135244913870580524E-13, -15.22848700163195623 ) ) ;
#186=CARTESIAN_POINT ( 'NONE',  ( 0.000000000000000000, 0.000000000000000000, 0.000000000000000000 ) ) ;
#199=CARTESIAN_POINT ( 'NONE',  ( -11.37500000000039613, -9.365624999999976552, 4.711679271993001628 ) ) ;
#215=CARTESIAN_POINT ( 'NONE',  ( 3.658660341103826763, -100.0000000000000000, 14.07150118901589408 ) ) ;
#217=CARTESIAN_POINT ( 'NONE',  ( 8.043339635996300530, -81.16874999999980389, 8.043339635997654113 ) ) ;
#227=CARTESIAN_POINT ( 'NONE',  ( -18.62500000000064659, -16.61562499999998010, 7.714727599197333419 ) ) ;
#233=CARTESIAN_POINT ( 'NONE',  ( -7.714727599197334307, -64.55312499999983800, -18.62500000000064659 ) ) ;
#235=CARTESIAN_POINT ( 'NONE',  ( 18.62499999999935341, -58.30937499999983231, 7.714727599200469577 ) ) ;
#257=CARTESIAN_POINT ( 'NONE',  ( 18.62500000000064304, -1.040624999999997469, -7.714727599197335195 ) ) ;
#258=CARTESIAN_POINT ( 'NONE',  ( -13.16986379959834252, -63.44374999999986642, -13.16986379960055409 ) ) ;
#270=CARTESIAN_POINT ( 'NONE',  ( 6.243927796512803496, 3.911145512478821826E-16, -15.59435523311979743 ) ) ;
#301=CARTESIAN_POINT ( 'NONE',  ( 4.711679271993006068, -46.82812499999989342, 11.37500000000039257 ) ) ;
#311=CARTESIAN_POINT ( 'NONE',  ( 7.714727599197340524, -70.72812499999984936, 18.62500000000063949 ) ) ;
#318=CARTESIAN_POINT ( 'NONE',  ( 13.16986379959833897, -73.91874999999977547, 13.16986379960055409 ) ) ;
#341=CARTESIAN_POINT ( 'NONE',  ( 13.16986379960055409, -75.93124999999983515, -13.16986379959834430 ) ) ;
#354=CARTESIAN_POINT ( 'NONE',  ( 8.083740994923175549, 5.967892910702088472E-16, -9.063702410685676725 ) ) ;
#371=CARTESIAN_POINT ( 'NONE',  ( 11.37500000000039435, -67.64062499999984368, -4.711679271993003404 ) ) ;
#390=CARTESIAN_POINT ( 'NONE',  ( -8.043339635997654113, -77.00624999999982379, 8.043339635996302306 ) ) ;
#399=CARTESIAN_POINT ( 'NONE',  ( -13.16986379959834252, -63.44374999999986642, -13.16986379960055409 ) ) ;
#407=CARTESIAN_POINT ( 'NONE',  ( 13.16986379959833897, -57.26874999999984794, 13.16986379960055409 ) ) ;
#412=CARTESIAN_POINT ( 'NONE',  ( 11.37500000000039435, -17.69062499999995453, -4.711679271993004292 ) ) ;
#431=CARTESIAN_POINT ( 'NONE',  ( 13.16986379960055409, -92.58124999999979821, -13.16986379959834430 ) ) ;
#442=CARTESIAN_POINT ( 'NONE',  ( 3.195015426203765330, 7.495012466571534215E-16, -14.06913727495813937 ) ) ;
#446=VECTOR ( 'NONE', #7079, 1000.000000000000000 ) ;
#458=CARTESIAN_POINT ( 'NONE',  ( 18.62499999999935341, -91.60937499999975842, 7.714727599200469577 ) ) ;
#459=CARTESIAN_POINT ( 'NONE',  ( -8.043339635997654113, -43.70624999999989768, 8.043339635996302306 ) ) ;
#466=CARTESIAN_POINT ( 'NONE',  ( -1.564113515457998572E-12, -12.48749999999997051, 18.62500000000000000 ) ) ;
#487=CARTESIAN_POINT ( 'NONE',  ( 7.714727599197340524, -37.42812499999993037, 18.62500000000063949 ) ) ;
#494=CARTESIAN_POINT ( 'NONE',  ( 1.561832610794586740E-12, -63.51249999999981810, -18.62500000000000000 ) ) ;
#502=CARTESIAN_POINT ( 'NONE',  ( -8.043339635996302306, -56.19374999999985931, -8.043339635997654113 ) ) ;
#516=CARTESIAN_POINT ( 'NONE',  ( 18.62500000000064659, -91.54062499999980673, -7.714727599197336083 ) ) ;
#529=( LENGTH_UNIT ( ) NAMED_UNIT ( * ) SI_UNIT ( .MILLI., .METRE. ) );
#543=CARTESIAN_POINT ( 'NONE',  ( -8.043339635997654113, -19.80624999999993463, 8.043339635996304082 ) ) ;
#544=CARTESIAN_POINT ( 'NONE',  ( 8.043339635997654113, -52.03124999999987921, -8.043339635996304082 ) ) ;
#573=CARTESIAN_POINT ( 'NONE',  ( -18.62500000000064659, -26.01562499999994671, 7.714727599197335195 ) ) ;
#579=CARTESIAN_POINT ( 'NONE',  ( -11.37500000000000178, -67.67499999999981242, -9.545674412382054647E-13 ) ) ;
#586=CARTESIAN_POINT ( 'NONE',  ( -8.043339635996302306, -39.54374999999990337, -8.043339635997654113 ) ) ;
#603=CARTESIAN_POINT ( 'NONE',  ( 18.62500000000000000, -107.1499999999997783, 1.560692158462880521E-12 ) ) ;
#630=CARTESIAN_POINT ( 'NONE',  ( 18.62500000000064659, -77.04062499999979252, -7.714727599197336083 ) ) ;
#631=CARTESIAN_POINT ( 'NONE',  ( 11.37499999999960210, -48.90937499999988347, 4.711679271994917428 ) ) ;
#634=CARTESIAN_POINT ( 'NONE',  ( 18.62500000000064304, -84.29062499999980673, -7.714727599197334307 ) ) ;
#657=CARTESIAN_POINT ( 'NONE',  ( 7.714727599200458030, -36.42187499999990763, -18.62499999999934985 ) ) ;
#666=CARTESIAN_POINT ( 'NONE',  ( -8.043339635997654113, -19.80624999999993463, 8.043339635996304082 ) ) ;
#674=CARTESIAN_POINT ( 'NONE',  ( 11.37500000000000000, -99.89999999999976410, 9.531744055041752924E-13 ) ) ;
#688=CARTESIAN_POINT ( 'NONE',  ( -13.16986379960055231, -43.70624999999989768, 13.16986379959834252 ) ) ;
#690=CARTESIAN_POINT ( 'NONE',  ( 18.62500000000064304, -34.34062499999991047, -7.714727599197335195 ) ) ;
#709=CARTESIAN_POINT ( 'NONE',  ( -4.711679271993001628, -12.45312499999998757, -11.37500000000039613 ) ) ;
#719=CARTESIAN_POINT ( 'NONE',  ( 8.043339635996302306, -23.96874999999992539, 8.043339635997654113 ) ) ;
#725=CARTESIAN_POINT ( 'NONE',  ( -18.62499999999935341, -57.23437499999987921, -7.714727599200458918 ) ) ;
#747=CARTESIAN_POINT ( 'NONE',  ( 18.62499999999934630, -15.60937499999996270, 7.714727599200467800 ) ) ;
#755=CARTESIAN_POINT ( 'NONE',  ( -11.37500000000000178, -51.02499999999986358, -9.545674412382054647E-13 ) ) ;
#762=CARTESIAN_POINT ( 'NONE',  ( 4.711679271993006068, -96.77812499999976126, 11.37500000000039257 ) ) ;
#775=CARTESIAN_POINT ( 'NONE',  ( -7.714727599197335195, -55.15312499999986784, -18.62500000000064304 ) ) ;
#777=CARTESIAN_POINT ( 'NONE',  ( 7.714727599197338748, -30.17812499999993747, 18.62500000000063949 ) ) ;
#790=CARTESIAN_POINT ( 'NONE',  ( -8.043339635997652337, -34.30624999999993463, 8.043339635996300530 ) ) ;
#799=CARTESIAN_POINT ( 'NONE',  ( 9.538709233711902776E-13, 3.087500000000011458, -11.37500000000000178 ) ) ;
#800=CARTESIAN_POINT ( 'NONE',  ( -9.552639591052204498E-13, -95.73749999999976978, 11.37500000000000000 ) ) ;
#803=CARTESIAN_POINT ( 'NONE',  ( 18.62499999999934985, -82.20937499999980957, 7.714727599200467800 ) ) ;
#823=CARTESIAN_POINT ( 'NONE',  ( -7.714727599197335195, -38.50312499999991189, -18.62500000000064304 ) ) ;
#833=CARTESIAN_POINT ( 'NONE',  ( 8.043339635997652337, -44.78124999999987921, -8.043339635996304082 ) ) ;
#840=CARTESIAN_POINT ( 'NONE',  ( 8.043339635996300530, -81.16874999999980389, 8.043339635997654113 ) ) ;
#850=CARTESIAN_POINT ( 'NONE',  ( 13.16986379959834075, -64.51874999999984084, 13.16986379960055231 ) ) ;
#852=CARTESIAN_POINT ( 'NONE',  ( -7.714727599200467800, -28.09687499999992966, 18.62499999999934630 ) ) ;
#854=CARTESIAN_POINT ( 'NONE',  ( 18.62499999999934630, -32.25937499999992042, 7.714727599200467800 ) ) ;
#873=CARTESIAN_POINT ( 'NONE',  ( 11.37499999999999645, -40.54999999999992610, 9.531744055041752924E-13 ) ) ;
#878=ORIENTED_EDGE ( 'NONE', *, *, #4542, .T. ) ;
#883=CARTESIAN_POINT ( 'NONE',  ( -4.711679271993003404, -47.90312499999986784, -11.37500000000039613 ) ) ;
#887=CARTESIAN_POINT ( 'NONE',  ( -18.62499999999935341, -90.53437499999978400, -7.714727599200458918 ) ) ;
#910=CARTESIAN_POINT ( 'NONE',  ( -1.564113515457998370E-12, -86.33749999999982094, 18.62500000000000000 ) ) ;
#921=CARTESIAN_POINT ( 'NONE',  ( 8.043339635997652337, -61.43124999999983515, -8.043339635996304082 ) ) ;
#929=CARTESIAN_POINT ( 'NONE',  ( -8.043339635996300530, -30.14374999999994742, -8.043339635997652337 ) ) ;
#938=CARTESIAN_POINT ( 'NONE',  ( -13.16986379959834252, -56.19374999999985931, -13.16986379960055054 ) ) ;
#940=CARTESIAN_POINT ( 'NONE',  ( -7.714727599200467800, -44.74687499999989626, 18.62499999999934630 ) ) ;
#942=CARTESIAN_POINT ( 'NONE',  ( 18.62500000000000000, -66.59999999999983800, 1.560692158462880521E-12 ) ) ;
#950=CARTESIAN_POINT ( 'NONE',  ( 11.37500000000000000, -9.629649721936179265E-32, 9.531744055041752924E-13 ) ) ;
#962=CARTESIAN_POINT ( 'NONE',  ( 11.37499999999960210, -56.15937499999989058, 4.711679271994916540 ) ) ;
#972=CARTESIAN_POINT ( 'NONE',  ( -4.711679271994916540, -37.49687499999989626, 11.37499999999960565 ) ) ;
#973=CARTESIAN_POINT ( 'NONE',  ( -11.37500000000000000, -91.57499999999977547, -9.545674412382054647E-13 ) ) ;
#1000=CARTESIAN_POINT ( 'NONE',  ( 18.62500000000000000, -83.24999999999980105, 1.560692158462880521E-12 ) ) ;
#1009=CARTESIAN_POINT ( 'NONE',  ( 8.047696313746376617, -99.99999999999994316, 9.235391612970973441 ) ) ;
#1010=DIRECTION ( 'NONE',  ( 0.000000000000000000, 0.000000000000000000, 1.000000000000000000 ) ) ;
#1011=CARTESIAN_POINT ( 'NONE',  ( 11.37500000000000178, -75.99999999999980105, 9.531744055041752924E-13 ) ) ;
#1021=CARTESIAN_POINT ( 'NONE',  ( -11.37499999999999645, -48.87499999999990052, -9.545674412382054647E-13 ) ) ;
#1028=CARTESIAN_POINT ( 'NONE',  ( 7.714727599197338748, -96.77812499999976126, 18.62500000000063949 ) ) ;
#1030=CARTESIAN_POINT ( 'NONE',  ( -13.16986379960055231, -77.00624999999982379, 13.16986379959834252 ) ) ;
#1034=CARTESIAN_POINT ( 'NONE',  ( -7.714727599197335195, -21.85312499999995239, -18.62500000000064304 ) ) ;
#1041=DIRECTION ( 'NONE',  ( 0.000000000000000000, 1.000000000000000000, 0.000000000000000000 ) ) ;
#1051=CARTESIAN_POINT ( 'NONE',  ( -11.37500000000039613, -49.91562499999989910, 4.711679271993000739 ) ) ;
#1060=CARTESIAN_POINT ( 'NONE',  ( 4.711679271993006957, -89.52812499999977547, 11.37500000000039613 ) ) ;
#1087=CARTESIAN_POINT ( 'NONE',  ( 18.62499999999934630, -65.55937499999984652, 7.714727599200467800 ) ) ;
#1097=CARTESIAN_POINT ( 'NONE',  ( -9.552639591052204498E-13, -12.48749999999997051, 11.37500000000000000 ) ) ;
#1105=CARTESIAN_POINT ( 'NONE',  ( -8.043339635997652337, -100.9062499999997868, 8.043339635996300530 ) ) ;
#1115=CARTESIAN_POINT ( 'NONE',  ( -18.62500000000064659, -92.61562499999978115, 7.714727599197335195 ) ) ;
#1117=CARTESIAN_POINT ( 'NONE',  ( 13.16986379959833897, -7.318749999999964118, 13.16986379960055409 ) ) ;
#1120=CARTESIAN_POINT ( 'NONE',  ( 13.16986379960055054, -85.33124999999978400, -13.16986379959834430 ) ) ;
#1138=CARTESIAN_POINT ( 'NONE',  ( 9.538709233711902776E-13, -61.36249999999986215, -11.37499999999999645 ) ) ;
#1148=CARTESIAN_POINT ( 'NONE',  ( -8.043339635997654113, -53.10624999999986073, 8.043339635996304082 ) ) ;
#1149=CARTESIAN_POINT ( 'NONE',  ( 13.16986379960055054, -18.73124999999995666, -13.16986379959834430 ) ) ;
#1175=CARTESIAN_POINT ( 'NONE',  ( -13.16986379960055231, -77.00624999999982379, 13.16986379959834252 ) ) ;
#1186=CARTESIAN_POINT ( 'NONE',  ( 11.37499999999960210, -32.25937499999992042, 4.711679271994918317 ) ) ;
#1195=CARTESIAN_POINT ( 'NONE',  ( -4.711679271994915652, -101.9468749999997783, 11.37499999999960210 ) ) ;
#1201=CARTESIAN_POINT ( 'NONE',  ( -18.62499999999934985, -73.88437499999982094, -7.714727599200458918 ) ) ;
#1203=CARTESIAN_POINT ( 'NONE',  ( -7.714727599197334307, -31.25312499999991545, -18.62500000000064659 ) ) ;
#1223=CARTESIAN_POINT ( 'NONE',  ( -8.043339635997652337, -84.25624999999980957, 8.043339635996300530 ) ) ;
#1231=CARTESIAN_POINT ( 'NONE',  ( 4.711679271993006957, -56.22812499999984936, 11.37500000000039613 ) ) ;
#1251=CARTESIAN_POINT ( 'NONE',  ( 11.37500000000039435, -17.69062499999995808, -4.711679271993003404 ) ) ;
#1265=CARTESIAN_POINT ( 'NONE',  ( 3.675929408452784486, -99.99999999999997158, 14.71521157600635910 ) ) ;
#1267=CARTESIAN_POINT ( 'NONE',  ( 11.37499999999960565, -91.60937499999975842, 4.711679271994918317 ) ) ;
#1276=CARTESIAN_POINT ( 'NONE',  ( 11.37499999999999645, -107.1499999999997783, 9.531744055041752924E-13 ) ) ;
#1281=CARTESIAN_POINT ( 'NONE',  ( 13.16986379959833897, -40.61874999999988489, 13.16986379960055409 ) ) ;
#1283=CARTESIAN_POINT ( 'NONE',  ( 1.561832610794586740E-12, 3.087500000000011458, -18.62500000000000000 ) ) ;
#1305=CARTESIAN_POINT ( 'NONE',  ( 4.711679271993006957, -87.37812499999982663, 11.37500000000039257 ) ) ;
#1313=CARTESIAN_POINT ( 'NONE',  ( 4.711679271993006068, -13.52812499999996732, 11.37500000000039257 ) ) ;
#1314=CARTESIAN_POINT ( 'NONE',  ( -1.564113515457998572E-12, -45.78749999999988773, 18.62500000000000000 ) ) ;
#1332=CARTESIAN_POINT ( 'NONE',  ( 11.37500000000039435, -1.040624999999997025, -4.711679271993003404 ) ) ;
#1336=CARTESIAN_POINT ( 'NONE',  ( 13.16986379959834075, -47.86874999999988489, 13.16986379960055231 ) ) ;
#1348=CARTESIAN_POINT ( 'NONE',  ( 5.439017319324713107, -99.99999999999994316, 15.41596283236346032 ) ) ;
#1350=CARTESIAN_POINT ( 'NONE',  ( 4.711679271993006068, -13.52812499999996732, 11.37500000000039257 ) ) ;
#1359=CARTESIAN_POINT ( 'NONE',  ( 9.538709233711902776E-13, -78.01249999999981810, -11.37499999999999645 ) ) ;
#1368=CARTESIAN_POINT ( 'NONE',  ( 1.561832610794586740E-12, -30.21249999999990976, -18.62500000000000000 ) ) ;
#1370=CARTESIAN_POINT ( 'NONE',  ( -1.564113515457998370E-12, -21.88749999999992824, 18.62500000000000000 ) ) ;
#1373=CARTESIAN_POINT ( 'NONE',  ( -18.62500000000064659, -75.96562499999980389, 7.714727599197335195 ) ) ;
#1392=CARTESIAN_POINT ( 'NONE',  ( 18.62500000000064659, -24.94062499999996518, -7.714727599197336083 ) ) ;
#1401=CARTESIAN_POINT ( 'NONE',  ( 11.37500000000039435, -50.99062499999987352, -4.711679271993004292 ) ) ;
#1402=CARTESIAN_POINT ( 'NONE',  ( -13.16986379960055231, -27.05624999999993463, 13.16986379959834252 ) ) ;
#1407=CARTESIAN_POINT ( 'NONE',  ( 6.278630761140489902, 1.381986750647006550E-15, -11.02614667217763511 ) ) ;
#1436=CARTESIAN_POINT ( 'NONE',  ( 18.55057311700109324, -99.99999999999998579, 1.729945603080623062 ) ) ;
#1438=CARTESIAN_POINT ( 'NONE',  ( 11.37499999999960210, -48.90937499999989058, 4.711679271994918317 ) ) ;
#1449=CARTESIAN_POINT ( 'NONE',  ( -4.711679271993001628, -79.05312499999985221, -11.37500000000039613 ) ) ;
#1456=CARTESIAN_POINT ( 'NONE',  ( 13.16986379960055409, -11.48124999999995488, -13.16986379959834430 ) ) ;
#1458=CARTESIAN_POINT ( 'NONE',  ( 18.62500000000064659, -10.44062499999995453, -7.714727599197336083 ) ) ;
#1484=CARTESIAN_POINT ( 'NONE',  ( 18.62500000000000000, -40.54999999999992610, 1.560692158462880521E-12 ) ) ;
#1494=CARTESIAN_POINT ( 'NONE',  ( -18.62499999999934985, -23.93437499999993889, -7.714727599200458918 ) ) ;
#1498=CARTESIAN_POINT ( 'NONE',  ( 13.94865728765873492, -5.025561147604149903E-16, -11.57659991980615644 ) ) ;
#1512=CARTESIAN_POINT ( 'NONE',  ( -8.043339635997654113, -10.40624999999997513, 8.043339635996302306 ) ) ;
#1518=CARTESIAN_POINT ( 'NONE',  ( -18.62499999999935341, -23.93437499999994245, -7.714727599200458918 ) ) ;
#1525=DIRECTION ( 'NONE',  ( -8.379555213223520053E-14, 0.000000000000000000, 1.000000000000000000 ) ) ;
#1527=CARTESIAN_POINT ( 'NONE',  ( 5.004910567252390585, -99.99999999999995737, 15.37359115544943577 ) ) ;
#1529=CARTESIAN_POINT ( 'NONE',  ( -11.37499999999960387, -90.53437499999978400, -4.711679271994910323 ) ) ;
#1538=CARTESIAN_POINT ( 'NONE',  ( -7.714727599197334307, -29.10312499999994884, -18.62500000000064659 ) ) ;
#1544=CARTESIAN_POINT ( 'NONE',  ( 18.62499999999935341, -41.65937499999989058, 7.714727599200469577 ) ) ;
#1546=CARTESIAN_POINT ( 'NONE',  ( -18.62500000000064659, -85.36562499999978115, 7.714727599197333419 ) ) ;
#1570=CARTESIAN_POINT ( 'NONE',  ( 4.711679271993006957, -104.0281249999997755, 11.37500000000039257 ) ) ;
#1583=CARTESIAN_POINT ( 'NONE',  ( 6.913829868824056035, -7.609836600491605532E-16, -10.40368044132385528 ) ) ;
#1619=CARTESIAN_POINT ( 'NONE',  ( 11.37500000000000000, -49.94999999999988205, 9.531744055041752924E-13 ) ) ;
#1627=CARTESIAN_POINT ( 'NONE',  ( -7.714727599197334307, -45.75312499999991189, -18.62500000000064659 ) ) ;
#1635=CARTESIAN_POINT ( 'NONE',  ( -13.16986379960055409, -53.10624999999986073, 13.16986379959834252 ) ) ;
#1658=CARTESIAN_POINT ( 'NONE',  ( -18.62500000000064659, -66.56562499999988347, 7.714727599197333419 ) ) ;
#1671=CARTESIAN_POINT ( 'NONE',  ( 3.514200034013206242, -6.916538280675000357E-15, -13.60917144867016404 ) ) ;
#1685=CARTESIAN_POINT ( 'NONE',  ( 11.37500000000000000, -49.94999999999988205, 9.531744055041752924E-13 ) ) ;
#1705=CARTESIAN_POINT ( 'NONE',  ( -11.37500000000039613, -42.66562499999989200, 4.711679271993002516 ) ) ;
#1716=CARTESIAN_POINT ( 'NONE',  ( 13.16986379959833897, -38.46874999999992895, 13.16986379960055409 ) ) ;
#1722=CARTESIAN_POINT ( 'NONE',  ( 7.714727599197340524, -56.22812499999984936, 18.62500000000063949 ) ) ;
#1728=CARTESIAN_POINT ( 'NONE',  ( 4.711679271993006068, -63.47812499999984226, 11.37500000000039257 ) ) ;
#1747=CARTESIAN_POINT ( 'NONE',  ( 7.714727599200456254, -93.62187499999978968, -18.62499999999935341 ) ) ;
#1760=CARTESIAN_POINT ( 'NONE',  ( 7.126290347628621902, 3.911145512478425917E-16, -15.45937452924531286 ) ) ;
#1775=CARTESIAN_POINT ( 'NONE',  ( -8.043339635996302306, -72.84374999999981526, -8.043339635997654113 ) ) ;
#1798=CARTESIAN_POINT ( 'NONE',  ( -18.62500000000000000, -65.52499999999986358, -1.562973063126292757E-12 ) ) ;
#1804=CARTESIAN_POINT ( 'NONE',  ( 8.043339635997652337, 5.168750000000006395, -8.043339635996304082 ) ) ;
#1811=CARTESIAN_POINT ( 'NONE',  ( 11.37499999999960210, -48.90937499999989058, 4.711679271994918317 ) ) ;
#1826=CARTESIAN_POINT ( 'NONE',  ( 18.62499999999935341, -89.45937499999983800, 7.714727599200469577 ) ) ;
#1856=CARTESIAN_POINT ( 'NONE',  ( -11.37500000000039790, -18.76562499999993605, 4.711679271993001628 ) ) ;
#1857=CARTESIAN_POINT ( 'NONE',  ( 8.043339635997654113, -85.33124999999978400, -8.043339635996304082 ) ) ;
#1863=CARTESIAN_POINT ( 'NONE',  ( 18.62500000000064304, -17.69062499999995808, -7.714727599197334307 ) ) ;
#1882=CARTESIAN_POINT ( 'NONE',  ( 13.16986379960055409, -25.98124999999995310, -13.16986379959834430 ) ) ;
#1891=CARTESIAN_POINT ( 'NONE',  ( 7.714727599197340524, -72.87812499999979821, 18.62500000000063949 ) ) ;
#1893=ORIENTED_EDGE ( 'NONE', *, *, #4756, .F. ) ;
#1897=CARTESIAN_POINT ( 'NONE',  ( -11.37500000000039613, -75.96562499999980389, 4.711679271993002516 ) ) ;
#1914=CARTESIAN_POINT ( 'NONE',  ( -1.564113515457998370E-12, -69.68749999999984368, 18.62500000000000000 ) ) ;
#1940=CARTESIAN_POINT ( 'NONE',  ( 11.37499999999960565, -25.00937499999992397, 4.711679271994918317 ) ) ;
#1941=CARTESIAN_POINT ( 'NONE',  ( -11.37500000000039613, -26.01562499999994316, 4.711679271993001628 ) ) ;
#1945=CARTESIAN_POINT ( 'NONE',  ( -7.714727599197334307, -55.15312499999986784, -18.62500000000064304 ) ) ;
#1953=( NAMED_UNIT ( * ) PLANE_ANGLE_UNIT ( ) SI_UNIT ( $, .RADIAN. ) );
#1966=CARTESIAN_POINT ( 'NONE',  ( 7.714727599197340524, -87.37812499999982663, 18.62500000000063949 ) ) ;
#1974=CARTESIAN_POINT ( 'NONE',  ( 8.043339635997652337, -11.48124999999995488, -8.043339635996304082 ) ) ;
#1981=CARTESIAN_POINT ( 'NONE',  ( -11.37499999999960210, -31.18437499999994245, -4.711679271994911211 ) ) ;
#1996=CARTESIAN_POINT ( 'NONE',  ( 18.62500000000000000, -33.29999999999991900, 1.560692158462880521E-12 ) ) ;
#1999=CARTESIAN_POINT ( 'NONE',  ( 18.62500000000000000, -57.19999999999988916, 1.560692158462880521E-12 ) ) ;
#2016=CARTESIAN_POINT ( 'NONE',  ( 4.711679271994911211, -10.37187499999999396, -11.37499999999960210 ) ) ;
#2027=CARTESIAN_POINT ( 'NONE',  ( 11.37500000000000178, -9.399999999999959499, 9.531744055041752924E-13 ) ) ;
#2028=CARTESIAN_POINT ( 'NONE',  ( -8.043339635997654113, -27.05624999999993463, 8.043339635996302306 ) ) ;
#2032=CARTESIAN_POINT ( 'NONE',  ( 13.16986379959834075, -47.86874999999988489, 13.16986379960055231 ) ) ;
#2054=CARTESIAN_POINT ( 'NONE',  ( 13.16986379959833897, -105.0687499999997527, 13.16986379960055409 ) ) ;
#2061=CARTESIAN_POINT ( 'NONE',  ( 11.37500000000039613, -27.09062499999992113, -4.711679271993004292 ) ) ;
#2066=ORIENTED_EDGE ( 'NONE', *, *, #2974, .F. ) ;
#2068=CARTESIAN_POINT ( 'NONE',  ( -11.37500000000039613, -92.61562499999978115, 4.711679271993002516 ) ) ;
#2080=CARTESIAN_POINT ( 'NONE',  ( 18.62499999999934630, -15.60937499999996270, 7.714727599200467800 ) ) ;
#2082=CARTESIAN_POINT ( 'NONE',  ( 18.62500000000064304, -50.99062499999987352, -7.714727599197335195 ) ) ;
#2099=CARTESIAN_POINT ( 'NONE',  ( -8.043339635997652337, -50.95624999999989768, 8.043339635996300530 ) ) ;
#2108=CARTESIAN_POINT ( 'NONE',  ( -11.37499999999960743, -0.03437499999998146899, -4.711679271994912099 ) ) ;
#2114=CARTESIAN_POINT ( 'NONE',  ( 13.16986379959834075, -81.16874999999980389, 13.16986379960055231 ) ) ;
#2135=CARTESIAN_POINT ( 'NONE',  ( -18.62500000000000000, -8.324999999999979750, -1.562973063126292555E-12 ) ) ;
#2148=CARTESIAN_POINT ( 'NONE',  ( 8.043339635996302306, -23.96874999999992539, 8.043339635997654113 ) ) ;
#2155=CARTESIAN_POINT ( 'NONE',  ( 11.37499999999999645, -40.54999999999992610, 9.531744055041752924E-13 ) ) ;
#2164=CARTESIAN_POINT ( 'NONE',  ( -13.16986379960055231, -77.00624999999982379, 13.16986379959834252 ) ) ;
#2166=CARTESIAN_POINT ( 'NONE',  ( 7.714727599197338748, -63.47812499999984226, 18.62500000000063949 ) ) ;
#2168=CARTESIAN_POINT ( 'NONE',  ( -18.62500000000000000, -24.97499999999994102, -1.562973063126292555E-12 ) ) ;
#2186=CARTESIAN_POINT ( 'NONE',  ( -11.37499999999960210, -31.18437499999994245, -4.711679271994911211 ) ) ;
#2196=CARTESIAN_POINT ( 'NONE',  ( 11.37499999999960565, -74.95937499999980957, 4.711679271994918317 ) ) ;
#2201=CARTESIAN_POINT ( 'NONE',  ( -1.564113515457998572E-12, -62.43749999999985079, 18.62500000000000000 ) ) ;
#2223=CARTESIAN_POINT ( 'NONE',  ( 13.16986379959834075, -14.56874999999996589, 13.16986379960055231 ) ) ;
#2230=CARTESIAN_POINT ( 'NONE',  ( 9.744583183820527239, -100.0000000000000853, 6.703353853222205672 ) ) ;
#2232=CARTESIAN_POINT ( 'NONE',  ( 11.37499999999960565, -58.30937499999983231, 4.711679271994918317 ) ) ;
#2240=CARTESIAN_POINT ( 'NONE',  ( 8.043339635997654113, -85.33124999999978400, -8.043339635996304082 ) ) ;
#2249=CARTESIAN_POINT ( 'NONE',  ( 7.714727599200456254, 4.128125000000008704, -18.62499999999935341 ) ) ;
#2251=CARTESIAN_POINT ( 'NONE',  ( 18.62500000000064304, -50.99062499999987352, -7.714727599197335195 ) ) ;
#2253=CARTESIAN_POINT ( 'NONE',  ( 7.714727599197338748, -63.47812499999984226, 18.62500000000063949 ) ) ;
#2273=CARTESIAN_POINT ( 'NONE',  ( 11.37499999999960210, -72.80937499999984652, 4.711679271994916540 ) ) ;
#2282=CARTESIAN_POINT ( 'NONE',  ( -8.043339635996302306, -6.243749999999984368, -8.043339635997654113 ) ) ;
#2285=CARTESIAN_POINT ( 'NONE',  ( -1.564113515457998572E-12, -29.13749999999993179, 18.62500000000000000 ) ) ;
#2309=CARTESIAN_POINT ( 'NONE',  ( -13.16986379959834252, -96.74374999999980673, -13.16986379960055409 ) ) ;
#2318=CARTESIAN_POINT ( 'NONE',  ( 8.833428499591450489, -99.99999999999995737, 8.182135825729266898 ) ) ;
#2320=CARTESIAN_POINT ( 'NONE',  ( 4.711679271994909435, -19.77187499999995168, -11.37499999999960387 ) ) ;
#2329=CARTESIAN_POINT ( 'NONE',  ( -11.37499999999960210, -47.83437499999990195, -4.711679271994911211 ) ) ;
#2336=APPLICATION_CONTEXT ( 'automotive_design' ) ;
#2337=CARTESIAN_POINT ( 'NONE',  ( 18.62500000000000000, -66.59999999999983800, 1.560692158462880521E-12 ) ) ;
#2339=CARTESIAN_POINT ( 'NONE',  ( -7.714727599197335195, -21.85312499999995239, -18.62500000000064304 ) ) ;
#2342=CARTESIAN_POINT ( 'NONE',  ( -18.62499999999934985, -57.23437499999987921, -7.714727599200458918 ) ) ;
#2360=CARTESIAN_POINT ( 'NONE',  ( -11.37499999999999645, -48.87499999999990052, -9.545674412382054647E-13 ) ) ;
#2370=CARTESIAN_POINT ( 'NONE',  ( -8.043339635997654113, -86.40624999999977263, 8.043339635996304082 ) ) ;
#2394=CARTESIAN_POINT ( 'NONE',  ( 13.16986379959834075, -97.81874999999976694, 13.16986379960055231 ) ) ;
#2402=CARTESIAN_POINT ( 'NONE',  ( -8.043339635997654113, -10.40624999999997513, 8.043339635996302306 ) ) ;
#2412=CARTESIAN_POINT ( 'NONE',  ( 8.043339635996298753, -71.76874999999985505, 8.043339635997652337 ) ) ;
#2418=CARTESIAN_POINT ( 'NONE',  ( 1.561832610794586538E-12, -87.41249999999979536, -18.62500000000000000 ) ) ;
#2420=CARTESIAN_POINT ( 'NONE',  ( 7.714727599200456254, 4.128125000000008704, -18.62499999999935341 ) ) ;
#2423=CARTESIAN_POINT ( 'NONE',  ( 13.16986379959834075, -31.21874999999992539, 13.16986379960055231 ) ) ;
#2442=CARTESIAN_POINT ( 'NONE',  ( -11.37499999999999645, -15.57499999999997975, -9.545674412382054647E-13 ) ) ;
#2452=EDGE_LOOP ( 'NONE', ( #2066, #15743, #16906, #8909, #878, #5361 ) ) ;
#2454=CARTESIAN_POINT ( 'NONE',  ( -11.37500000000039790, -85.36562499999978115, 4.711679271993001628 ) ) ;
#2479=CARTESIAN_POINT ( 'NONE',  ( -18.62499999999934985, -73.88437499999982094, -7.714727599200458918 ) ) ;
#2490=CARTESIAN_POINT ( 'NONE',  ( 11.37500000000000000, -33.29999999999991900, 9.531744055041752924E-13 ) ) ;
#2500=CARTESIAN_POINT ( 'NONE',  ( -9.552639591052204498E-13, -69.68749999999984368, 11.37499999999999645 ) ) ;
#2508=CARTESIAN_POINT ( 'NONE',  ( -1.564113515457998572E-12, -95.73749999999976978, 18.62500000000000000 ) ) ;
#2510=CARTESIAN_POINT ( 'NONE',  ( 13.16986379959833897, -23.96874999999992539, 13.16986379960055409 ) ) ;
#2513=CARTESIAN_POINT ( 'NONE',  ( 7.714727599197338748, -96.77812499999976126, 18.62500000000063949 ) ) ;
#2534=CARTESIAN_POINT ( 'NONE',  ( -11.37499999999999645, -98.82499999999978968, -9.545674412382054647E-13 ) ) ;
#2543=CARTESIAN_POINT ( 'NONE',  ( -8.043339635997654113, -69.75624999999980957, 8.043339635996304082 ) ) ;
#2544=CARTESIAN_POINT ( 'NONE',  ( -1.564113515457998572E-12, -29.13749999999993179, 18.62500000000000000 ) ) ;
#2564=CARTESIAN_POINT ( 'NONE',  ( -8.043339635996302306, -6.243749999999984368, -8.043339635997654113 ) ) ;
#2568=CARTESIAN_POINT ( 'NONE',  ( -7.714727599197335195, -88.45312499999978684, -18.62500000000064304 ) ) ;
#2577=CARTESIAN_POINT ( 'NONE',  ( 12.56770389185380665, -100.0000000000000426, 12.75622125074128910 ) ) ;
#2579=CARTESIAN_POINT ( 'NONE',  ( 11.37500000000000178, -92.64999999999974989, 9.531744055041752924E-13 ) ) ;
#2583=VERTEX_POINT ( 'NONE', #950 ) ;
#2584=ORIENTED_EDGE ( 'NONE', *, *, #12599, .F. ) ;
#2588=CARTESIAN_POINT ( 'NONE',  ( 8.043339635996298753, -105.0687499999997527, 8.043339635997652337 ) ) ;
#2595=CARTESIAN_POINT ( 'NONE',  ( -7.714727599200466912, -20.84687499999993321, 18.62499999999935341 ) ) ;
#2597=CARTESIAN_POINT ( 'NONE',  ( -13.16986379960055409, -3.156249999999973355, 13.16986379959834252 ) ) ;
#2600=CARTESIAN_POINT ( 'NONE',  ( 13.16986379959834075, -97.81874999999976694, 13.16986379960055231 ) ) ;
#2618=CARTESIAN_POINT ( 'NONE',  ( -18.62500000000000000, -32.22499999999993747, -1.562973063126292757E-12 ) ) ;
#2628=CARTESIAN_POINT ( 'NONE',  ( 11.37499999999960210, -32.25937499999992042, 4.711679271994918317 ) ) ;
#2629=CARTESIAN_POINT ( 'NONE',  ( -18.62500000000064659, -42.66562499999989200, 7.714727599197335195 ) ) ;
#2656=CARTESIAN_POINT ( 'NONE',  ( -18.62500000000064659, -75.96562499999980389, 7.714727599197335195 ) ) ;
#2666=FACE_OUTER_BOUND ( 'NONE', #17082, .T. ) ;
#2667=CARTESIAN_POINT ( 'NONE',  ( 9.538709233711902776E-13, -80.16249999999979536, -11.37500000000000178 ) ) ;
#2676=CARTESIAN_POINT ( 'NONE',  ( 8.043339635997652337, -75.93124999999983515, -8.043339635996302306 ) ) ;
#2683=CARTESIAN_POINT ( 'NONE',  ( -7.714727599197334307, -31.25312499999991545, -18.62500000000064659 ) ) ;
#2685=CARTESIAN_POINT ( 'NONE',  ( -7.714727599200466912, -4.196874999999971934, 18.62499999999935341 ) ) ;
#2708=CARTESIAN_POINT ( 'NONE',  ( 11.37499999999999645, -107.1499999999997783, 9.531744055041752924E-13 ) ) ;
#2717=CARTESIAN_POINT ( 'NONE',  ( -4.711679271994916540, -61.39687499999984510, 11.37499999999960210 ) ) ;
#2718=FACE_OUTER_BOUND ( 'NONE', #17231, .T. ) ;
#2745=FACE_OUTER_BOUND ( 'NONE', #4037, .T. ) ;
#2750=PLANE ( 'NONE',  #7593 ) ;
#2755=CARTESIAN_POINT ( 'NONE',  ( -4.711679271993004292, -71.80312499999982379, -11.37500000000039435 ) ) ;
#2763=CARTESIAN_POINT ( 'NONE',  ( -11.37500000000039613, -99.86562499999978115, 4.711679271993000739 ) ) ;
#2772=CARTESIAN_POINT ( 'NONE',  ( -18.62500000000064659, -52.06562499999986926, 7.714727599197333419 ) ) ;
#2774=CARTESIAN_POINT ( 'NONE',  ( 13.16986379960055409, -28.13124999999991260, -13.16986379959834430 ) ) ;
#2798=CARTESIAN_POINT ( 'NONE',  ( -4.711679271994915652, -85.29687499999980105, 11.37499999999960210 ) ) ;
#2806=CARTESIAN_POINT ( 'NONE',  ( 18.62500000000000000, -16.64999999999995950, 1.560692158462880521E-12 ) ) ;
#2812=CARTESIAN_POINT ( 'NONE',  ( 3.119116752841613938, 2.511656448626852424E-16, -14.83158588741119388 ) ) ;
#2834=CARTESIAN_POINT ( 'NONE',  ( -7.714727599197334307, -21.85312499999994884, -18.62500000000064304 ) ) ;
#2842=CARTESIAN_POINT ( 'NONE',  ( 3.856686604160783904, -100.0000000000000426, 13.67982212280359455 ) ) ;
#2844=CARTESIAN_POINT ( 'NONE',  ( -4.711679271994916540, -94.69687499999979252, 11.37499999999960210 ) ) ;
#2853=CARTESIAN_POINT ( 'NONE',  ( 18.62499999999935341, -56.15937499999989058, 7.714727599200469577 ) ) ;
#2861=CARTESIAN_POINT ( 'NONE',  ( -13.16986379959834252, -32.29374999999990337, -13.16986379960055409 ) ) ;
#2863=CARTESIAN_POINT ( 'NONE',  ( -7.714727599197334307, -47.90312499999986784, -18.62500000000064659 ) ) ;
#2886=CARTESIAN_POINT ( 'NONE',  ( 11.37500000000039613, -91.54062499999980673, -4.711679271993002516 ) ) ;
#2915=CARTESIAN_POINT ( 'NONE',  ( 4.711679271994910323, -3.121874999999992184, -11.37499999999960387 ) ) ;
#2933=CARTESIAN_POINT ( 'NONE',  ( -11.37500000000000000, -58.27499999999986358, -9.545674412382054647E-13 ) ) ;
#2934=LINE ( 'NONE', #16286, #13446 ) ;
#2945=CARTESIAN_POINT ( 'NONE',  ( 1.561832610794586740E-12, -28.06249999999995381, -18.62500000000000000 ) ) ;
#2950=PRODUCT ( 'Spring', 'Spring', '', ( #3873 ) ) ;
#2951=CARTESIAN_POINT ( 'NONE',  ( -18.62499999999935341, -49.98437499999987210, -7.714727599200458030 ) ) ;
#2954=CARTESIAN_POINT ( 'NONE',  ( 13.16986379960055409, -44.78124999999987921, -13.16986379959834430 ) ) ;
#2974=EDGE_CURVE ( 'NONE', #2583, #13643, #5827, .T. ) ;
#2976=CARTESIAN_POINT ( 'NONE',  ( 18.62499999999935341, -56.15937499999989058, 7.714727599200469577 ) ) ;
#2987=CARTESIAN_POINT ( 'NONE',  ( 17.50831196659380140, 3.710240846040484935E-14, -6.047149036516558773 ) ) ;
#2992=EDGE_CURVE ( 'NONE', #13643, #2583, #8587, .T. ) ;
#2993=DIRECTION ( 'NONE',  ( 1.000000000000000000, 0.000000000000000000, 0.000000000000000000 ) ) ;
#3003=CARTESIAN_POINT ( 'NONE',  ( -11.37500000000039613, -59.31562499999985505, 4.711679271993001628 ) ) ;
#3010=CARTESIAN_POINT ( 'NONE',  ( -18.62500000000000000, -8.324999999999979750, -1.562973063126292555E-12 ) ) ;
#3022=CARTESIAN_POINT ( 'NONE',  ( -8.043339635997654113, -93.65624999999977263, 8.043339635996302306 ) ) ;
#3032=CARTESIAN_POINT ( 'NONE',  ( 7.714727599200456254, -27.02187499999995524, -18.62499999999935341 ) ) ;
#3040=CARTESIAN_POINT ( 'NONE',  ( -13.16986379960055409, -69.75624999999980957, 13.16986379959834252 ) ) ;
#3047=CARTESIAN_POINT ( 'NONE',  ( 8.043339635996300530, -31.21874999999992539, 8.043339635997654113 ) ) ;
#3067=CARTESIAN_POINT ( 'NONE',  ( -7.714727599197334307, -79.05312499999985221, -18.62500000000064659 ) ) ;
#3069=( BOUNDED_SURFACE ( )  B_SPLINE_SURFACE ( 3, 2, ( 
 ( #11395, #257, #11218, #16680, #9995, #9820, #3243, #8666, #16767, #9642, #16416, #10166, #8921, #15686, #4760, #2080, #10417, #3426, #7423, #14198, #14363, #2339, #15600, #3593, #15514, #11824, #10247, #852, #10080, #3340, #6263, #14111, #1996, #4675, #7679, #11567, #15431, #12803, #6441, #9005, #8755, #13058, #688, #940, #6101, #11482, #16941, #16857, #12886, #2251, #6351, #7505, #8841, #775, #11735, #13143, #6181, #14452, #14280, #4843, #3508, #2166, #7591, #17113, #11650, #12970, #17027, #4931, #5018, #10332, #15775, #3686, #9099, #7772, #1030, #16036, #8205, #15867, #6697, #13228, #3774, #6614, #4120, #5370, #15952, #10757, #14708, #17456, #17288, #3944, #9187, #11994, #16120, #13567, #17376, #6878, #12164 ),
 ( #14793, #14535, #10505, #2420, #1283, #55, #7853, #4031, #3858, #9445, #2597, #2685, #5200, #9359, #1117, #5290, #8116, #1458, #10672, #17204, #5459, #6531, #9272, #12077, #13482, #11909, #10590, #14624, #1370, #10842, #2510, #7940, #13312, #14878, #2774, #5112, #6785, #1203, #8026, #13394, #16209, #9534, #5727, #11198, #10935, #8295, #4297, #9797, #5901, #11023, #2954, #16302, #9970, #2863, #11109, #12523, #16482, #6965, #1635, #15143, #16657, #1722, #407, #235, #4386, #5814, #12343, #9710, #494, #16395, #14973, #15054, #4479, #15318, #3040, #16574, #5641, #1891, #318, #8471, #146, #4209, #13821, #9622, #13652, #12251, #15235, #7052, #5552, #1546, #13996, #9885, #8382, #3131, #13737, #8556, #12432 ),
 ( #7135, #13909, #1804, #7218, #12605, #11280, #4564, #3221, #8643, #17093, #16921, #4737, #5989, #11544, #14087, #4913, #14258, #8729, #1974, #10057, #8987, #3489, #7398, #7572, #14176, #8818, #666, #6163, #15756, #11371, #2148, #3315, #16743, #2061, #11718, #12778, #5000, #4823, #10141, #4651, #10225, #6077, #10311, #12949, #11457, #16833, #15409, #14344, #8904, #15493, #833, #7485, #12866, #3404, #15580, #3666, #755, #6244, #11630, #17005, #15665, #10399, #3574, #2232, #7662, #13039, #921, #6329, #9078, #14431, #7306, #12691, #579, #14608, #9515, #14777, #15847, #11893, #9343, #17439, #1011, #13122, #6422, #3926, #2667, #11805, #7837, #17183, #33, #5439, #10826, #14692, #5094, #17358, #14516, #1267, #2579 ),
 ( #10486, #10740, #16188, #4100, #5271, #5180, #3754, #5353, #12144, #9168, #2402, #13210, #1097, #1350, #8098, #8011, #13464, #7922, #7748, #2320, #9255, #6679, #15933, #16104, #6512, #13296, #10656, #17268, #10572, #3839, #4014, #1186, #2490, #12062, #9428, #6596, #11976, #16019, #13378, #6766, #125, #1705, #12324, #4369, #13720, #301, #10915, #1438, #1619, #11499, #14954, #11093, #12234, #8363, #16284, #6945, #2933, #7443, #7036, #8187, #13548, #3358, #4191, #13636, #14129, #15449, #16465, #8774, #12414, #2755, #14860, #4280, #13807, #11004, #390, #9604, #5711, #9778, #217, #16875, #5623, #11180, #15124, #4780, #7118, #12505, #6856, #1529, #16375, #5531, #3022, #2844, #5796, #9690, #8453, #16555, #4462 ),
 ( #8275, #15039, #9867, #2016, #12822, #709, #6119, #15710, #2442, #9028, #3445, #8862, #15887, #16962, #10183, #4864, #10267, #12906, #13076, #15534, #3705, #7874, #17309, #2186, #9122, #14214, #790, #9207, #3527, #7793, #8942, #11586, #873, #7699, #6463, #13164, #14300, #3795, #6549, #12990, #2360, #1051, #2099, #13251, #11928, #14559, #10524, #962, #14472, #7614, #11848, #3614, #1138, #6200, #6284, #10441, #11672, #17047, #7526, #4953, #10356, #15619, #14384, #2273, #17223, #6374, #11758, #17134, #5044, #15800, #5133, #13415, #17395, #171, #1223, #2798, #12185, #1305, #15975, #9294, #13590, #2886, #6989, #8137, #8048, #6636, #8229, #14994, #2534, #3878, #14646, #8318, #13673, #1570, #77, #7962, #2708 ),
 ( #16142, #4141, #13332, #12015, #14729, #13502, #16326, #3968, #6719, #5311, #12364, #10694, #4052, #5482, #9466, #16060, #12097, #1392, #9644, #10864, #16232, #9380, #14813, #9554, #2618, #17479, #10958, #5393, #10778, #6807, #14904, #5222, #1484, #6901, #12274, #10608, #5576, #4233, #5666, #16418, #13932, #9730, #15076, #7425, #3245, #7159, #11046, #2976, #1999, #16682, #4320, #8668, #8406, #14025, #258, #13758, #12544, #1658, #8494, #4589, #1914, #9823, #7073, #15168, #7333, #8757, #341, #10082, #9909, #3067, #12457, #4502, #5750, #15344, #7242, #11134, #16507, #4412, #12717, #1826, #13845, #516, #431, #1747, #5837, #16595, #14113, #11220, #12628, #15256, #3154, #8581, #4677, #5925, #11304, #9996, #603 ),
 ( #6014, #11397, #16769, #15433, #3343, #8844, #6184, #13060, #4845, #15603, #11828, #10249, #11569, #5115, #7594, #3510, #9102, #16943, #6353, #12888, #8923, #1034, #14282, #15516, #2168, #5021, #10508, #6265, #11738, #777, #2423, #854, #9008, #690, #11484, #14365, #4763, #10168, #12805, #15778, #12972, #6103, #3428, #14538, #17115, #16859, #3689, #14200, #14455, #2082, #7507, #11652, #17029, #4934, #10420, #2342, #10334, #15688, #3595, #7774, #3777, #2253, #15870, #7681, #942, #13146, #6443, #17206, #9189, #17460, #15954, #9275, #17290, #1373, #6699, #3861, #5373, #10675, #5293, #7942, #14712, #14881, #1120, #10760, #14628, #6533, #16040, #16211, #16123, #13315, #4034, #13397, #9448, #2513, #2600, #11912, #3948 ) ),
 .UNSPECIFIED., .T., .F., .F. ) 
 B_SPLINE_SURFACE_WITH_KNOTS ( ( 4, 3, 4 ),
 ( 3, 2, 2, 2, 2, 2, 2, 2, 2, 2, 2, 2, 2, 2, 2, 2, 2, 2, 2, 2, 2, 2, 2, 2, 2, 2, 2, 2, 2, 2, 2, 2, 2, 2, 2, 2, 2, 2, 2, 2, 2, 2, 2, 2, 2, 2, 2, 2, 3 ),
 ( 0.000000000000000000, 0.5000000000000000000, 1.000000000000000000 ),
 ( 0.000000000000000000, 0.02083333333333333218, 0.04166666666666666435, 0.06250000000000000000, 0.08333333333333332871, 0.1041666666666666713, 0.1250000000000000000, 0.1458333333333333426, 0.1666666666666666574, 0.1875000000000000000, 0.2083333333333333426, 0.2291666666666666574, 0.2500000000000000000, 0.2708333333333333148, 0.2916666666666666852, 0.3125000000000000000, 0.3333333333333333148, 0.3541666666666666852, 0.3750000000000000000, 0.3958333333333333148, 0.4166666666666666852, 0.4375000000000000000, 0.4583333333333333148, 0.4791666666666666852, 0.5000000000000000000, 0.5208333333333333703, 0.5416666666666666297, 0.5625000000000000000, 0.5833333333333333703, 0.6041666666666666297, 0.6250000000000000000, 0.6458333333333333703, 0.6666666666666666297, 0.6875000000000000000, 0.7083333333333333703, 0.7291666666666666297, 0.7500000000000000000, 0.7708333333333333703, 0.7916666666666666297, 0.8125000000000000000, 0.8333333333333333703, 0.8541666666666666297, 0.8750000000000000000, 0.8958333333333333703, 0.9166666666666666297, 0.9375000000000000000, 0.9583333333333333703, 0.9791666666666666297, 1.000000000000000000 ),
 .UNSPECIFIED. ) 
 GEOMETRIC_REPRESENTATION_ITEM ( )  RATIONAL_B_SPLINE_SURFACE ( (
 ( 1.000000000000000000, 0.9238795325112867385, 1.000000000000000000, 0.9238795325112867385, 1.000000000000000000, 0.9238795325112867385, 1.000000000000000000, 0.9238795325112867385, 1.000000000000000000, 0.9238795325112867385, 1.000000000000000000, 0.9238795325112867385, 1.000000000000000000, 0.9238795325112867385, 1.000000000000000000, 0.9238795325112867385, 1.000000000000000000, 0.9238795325112867385, 1.000000000000000000, 0.9238795325112867385, 1.000000000000000000, 0.9238795325112867385, 1.000000000000000000, 0.9238795325112867385, 1.000000000000000000, 0.9238795325112867385, 1.000000000000000000, 0.9238795325112867385, 1.000000000000000000, 0.9238795325112867385, 1.000000000000000000, 0.9238795325112867385, 1.000000000000000000, 0.9238795325112867385, 1.000000000000000000, 0.9238795325112867385, 1.000000000000000000, 0.9238795325112867385, 1.000000000000000000, 0.9238795325112867385, 1.000000000000000000, 0.9238795325112867385, 1.000000000000000000, 0.9238795325112867385, 1.000000000000000000, 0.9238795325112867385, 1.000000000000000000, 0.9238795325112867385, 1.000000000000000000, 0.9238795325112867385, 1.000000000000000000, 0.9238795325112867385, 1.000000000000000000, 0.9238795325112867385, 1.000000000000000000, 0.9238795325112867385, 1.000000000000000000, 0.9238795325112867385, 1.000000000000000000, 0.9238795325112867385, 1.000000000000000000, 0.9238795325112867385, 1.000000000000000000, 0.9238795325112867385, 1.000000000000000000, 0.9238795325112867385, 1.000000000000000000, 0.9238795325112867385, 1.000000000000000000, 0.9238795325112867385, 1.000000000000000000, 0.9238795325112867385, 1.000000000000000000, 0.9238795325112867385, 1.000000000000000000, 0.9238795325112867385, 1.000000000000000000, 0.9238795325112867385, 1.000000000000000000, 0.9238795325112867385, 1.000000000000000000, 0.9238795325112867385, 1.000000000000000000, 0.9238795325112867385, 1.000000000000000000, 0.9238795325112867385, 1.000000000000000000, 0.9238795325112867385, 1.000000000000000000, 0.9238795325112867385, 1.000000000000000000, 0.9238795325112867385, 1.000000000000000000, 0.9238795325112867385, 1.000000000000000000, 0.9238795325112867385, 1.000000000000000000),
 ( 0.3333333333333333703, 0.3079598441704289313, 0.3333333333333333703, 0.3079598441704289313, 0.3333333333333333703, 0.3079598441704289313, 0.3333333333333333703, 0.3079598441704289313, 0.3333333333333333703, 0.3079598441704289313, 0.3333333333333333703, 0.3079598441704289313, 0.3333333333333333703, 0.3079598441704289313, 0.3333333333333333703, 0.3079598441704289313, 0.3333333333333333703, 0.3079598441704289313, 0.3333333333333333703, 0.3079598441704289313, 0.3333333333333333703, 0.3079598441704289313, 0.3333333333333333703, 0.3079598441704289313, 0.3333333333333333703, 0.3079598441704289313, 0.3333333333333333703, 0.3079598441704289313, 0.3333333333333333703, 0.3079598441704289313, 0.3333333333333333703, 0.3079598441704289313, 0.3333333333333333703, 0.3079598441704289313, 0.3333333333333333703, 0.3079598441704289313, 0.3333333333333333703, 0.3079598441704289313, 0.3333333333333333703, 0.3079598441704289313, 0.3333333333333333703, 0.3079598441704289313, 0.3333333333333333703, 0.3079598441704289313, 0.3333333333333333703, 0.3079598441704289313, 0.3333333333333333703, 0.3079598441704289313, 0.3333333333333333703, 0.3079598441704289313, 0.3333333333333333703, 0.3079598441704289313, 0.3333333333333333703, 0.3079598441704289313, 0.3333333333333333703, 0.3079598441704289313, 0.3333333333333333703, 0.3079598441704289313, 0.3333333333333333703, 0.3079598441704289313, 0.3333333333333333703, 0.3079598441704289313, 0.3333333333333333703, 0.3079598441704289313, 0.3333333333333333703, 0.3079598441704289313, 0.3333333333333333703, 0.3079598441704289313, 0.3333333333333333703, 0.3079598441704289313, 0.3333333333333333703, 0.3079598441704289313, 0.3333333333333333703, 0.3079598441704289313, 0.3333333333333333703, 0.3079598441704289313, 0.3333333333333333703, 0.3079598441704289313, 0.3333333333333333703, 0.3079598441704289313, 0.3333333333333333703, 0.3079598441704289313, 0.3333333333333333703, 0.3079598441704289313, 0.3333333333333333703, 0.3079598441704289313, 0.3333333333333333703, 0.3079598441704289313, 0.3333333333333333703, 0.3079598441704289313, 0.3333333333333333703, 0.3079598441704289313, 0.3333333333333333703, 0.3079598441704289313, 0.3333333333333333703, 0.3079598441704289313, 0.3333333333333333703),
 ( 0.3333333333333333703, 0.3079598441704289313, 0.3333333333333333703, 0.3079598441704289313, 0.3333333333333333703, 0.3079598441704289313, 0.3333333333333333703, 0.3079598441704289313, 0.3333333333333333703, 0.3079598441704289313, 0.3333333333333333703, 0.3079598441704289313, 0.3333333333333333703, 0.3079598441704289313, 0.3333333333333333703, 0.3079598441704289313, 0.3333333333333333703, 0.3079598441704289313, 0.3333333333333333703, 0.3079598441704289313, 0.3333333333333333703, 0.3079598441704289313, 0.3333333333333333703, 0.3079598441704289313, 0.3333333333333333703, 0.3079598441704289313, 0.3333333333333333703, 0.3079598441704289313, 0.3333333333333333703, 0.3079598441704289313, 0.3333333333333333703, 0.3079598441704289313, 0.3333333333333333703, 0.3079598441704289313, 0.3333333333333333703, 0.3079598441704289313, 0.3333333333333333703, 0.3079598441704289313, 0.3333333333333333703, 0.3079598441704289313, 0.3333333333333333703, 0.3079598441704289313, 0.3333333333333333703, 0.3079598441704289313, 0.3333333333333333703, 0.3079598441704289313, 0.3333333333333333703, 0.3079598441704289313, 0.3333333333333333703, 0.3079598441704289313, 0.3333333333333333703, 0.3079598441704289313, 0.3333333333333333703, 0.3079598441704289313, 0.3333333333333333703, 0.3079598441704289313, 0.3333333333333333703, 0.3079598441704289313, 0.3333333333333333703, 0.3079598441704289313, 0.3333333333333333703, 0.3079598441704289313, 0.3333333333333333703, 0.3079598441704289313, 0.3333333333333333703, 0.3079598441704289313, 0.3333333333333333703, 0.3079598441704289313, 0.3333333333333333703, 0.3079598441704289313, 0.3333333333333333703, 0.3079598441704289313, 0.3333333333333333703, 0.3079598441704289313, 0.3333333333333333703, 0.3079598441704289313, 0.3333333333333333703, 0.3079598441704289313, 0.3333333333333333703, 0.3079598441704289313, 0.3333333333333333703, 0.3079598441704289313, 0.3333333333333333703, 0.3079598441704289313, 0.3333333333333333703, 0.3079598441704289313, 0.3333333333333333703, 0.3079598441704289313, 0.3333333333333333703, 0.3079598441704289313, 0.3333333333333333703, 0.3079598441704289313, 0.3333333333333333703, 0.3079598441704289313, 0.3333333333333333703, 0.3079598441704289313, 0.3333333333333333703),
 ( 1.000000000000000000, 0.9238795325112867385, 1.000000000000000000, 0.9238795325112867385, 1.000000000000000000, 0.9238795325112867385, 1.000000000000000000, 0.9238795325112867385, 1.000000000000000000, 0.9238795325112867385, 1.000000000000000000, 0.9238795325112867385, 1.000000000000000000, 0.9238795325112867385, 1.000000000000000000, 0.9238795325112867385, 1.000000000000000000, 0.9238795325112867385, 1.000000000000000000, 0.9238795325112867385, 1.000000000000000000, 0.9238795325112867385, 1.000000000000000000, 0.9238795325112867385, 1.000000000000000000, 0.9238795325112867385, 1.000000000000000000, 0.9238795325112867385, 1.000000000000000000, 0.9238795325112867385, 1.000000000000000000, 0.9238795325112867385, 1.000000000000000000, 0.9238795325112867385, 1.000000000000000000, 0.9238795325112867385, 1.000000000000000000, 0.9238795325112867385, 1.000000000000000000, 0.9238795325112867385, 1.000000000000000000, 0.9238795325112867385, 1.000000000000000000, 0.9238795325112867385, 1.000000000000000000, 0.9238795325112867385, 1.000000000000000000, 0.9238795325112867385, 1.000000000000000000, 0.9238795325112867385, 1.000000000000000000, 0.9238795325112867385, 1.000000000000000000, 0.9238795325112867385, 1.000000000000000000, 0.9238795325112867385, 1.000000000000000000, 0.9238795325112867385, 1.000000000000000000, 0.9238795325112867385, 1.000000000000000000, 0.9238795325112867385, 1.000000000000000000, 0.9238795325112867385, 1.000000000000000000, 0.9238795325112867385, 1.000000000000000000, 0.9238795325112867385, 1.000000000000000000, 0.9238795325112867385, 1.000000000000000000, 0.9238795325112867385, 1.000000000000000000, 0.9238795325112867385, 1.000000000000000000, 0.9238795325112867385, 1.000000000000000000, 0.9238795325112867385, 1.000000000000000000, 0.9238795325112867385, 1.000000000000000000, 0.9238795325112867385, 1.000000000000000000, 0.9238795325112867385, 1.000000000000000000, 0.9238795325112867385, 1.000000000000000000, 0.9238795325112867385, 1.000000000000000000, 0.9238795325112867385, 1.000000000000000000, 0.9238795325112867385, 1.000000000000000000, 0.9238795325112867385, 1.000000000000000000, 0.9238795325112867385, 1.000000000000000000),
 ( 0.3333333333333333703, 0.3079598441704289313, 0.3333333333333333703, 0.3079598441704289313, 0.3333333333333333703, 0.3079598441704289313, 0.3333333333333333703, 0.3079598441704289313, 0.3333333333333333703, 0.3079598441704289313, 0.3333333333333333703, 0.3079598441704289313, 0.3333333333333333703, 0.3079598441704289313, 0.3333333333333333703, 0.3079598441704289313, 0.3333333333333333703, 0.3079598441704289313, 0.3333333333333333703, 0.3079598441704289313, 0.3333333333333333703, 0.3079598441704289313, 0.3333333333333333703, 0.3079598441704289313, 0.3333333333333333703, 0.3079598441704289313, 0.3333333333333333703, 0.3079598441704289313, 0.3333333333333333703, 0.3079598441704289313, 0.3333333333333333703, 0.3079598441704289313, 0.3333333333333333703, 0.3079598441704289313, 0.3333333333333333703, 0.3079598441704289313, 0.3333333333333333703, 0.3079598441704289313, 0.3333333333333333703, 0.3079598441704289313, 0.3333333333333333703, 0.3079598441704289313, 0.3333333333333333703, 0.3079598441704289313, 0.3333333333333333703, 0.3079598441704289313, 0.3333333333333333703, 0.3079598441704289313, 0.3333333333333333703, 0.3079598441704289313, 0.3333333333333333703, 0.3079598441704289313, 0.3333333333333333703, 0.3079598441704289313, 0.3333333333333333703, 0.3079598441704289313, 0.3333333333333333703, 0.3079598441704289313, 0.3333333333333333703, 0.3079598441704289313, 0.3333333333333333703, 0.3079598441704289313, 0.3333333333333333703, 0.3079598441704289313, 0.3333333333333333703, 0.3079598441704289313, 0.3333333333333333703, 0.3079598441704289313, 0.3333333333333333703, 0.3079598441704289313, 0.3333333333333333703, 0.3079598441704289313, 0.3333333333333333703, 0.3079598441704289313, 0.3333333333333333703, 0.3079598441704289313, 0.3333333333333333703, 0.3079598441704289313, 0.3333333333333333703, 0.3079598441704289313, 0.3333333333333333703, 0.3079598441704289313, 0.3333333333333333703, 0.3079598441704289313, 0.3333333333333333703, 0.3079598441704289313, 0.3333333333333333703, 0.3079598441704289313, 0.3333333333333333703, 0.3079598441704289313, 0.3333333333333333703, 0.3079598441704289313, 0.3333333333333333703, 0.3079598441704289313, 0.3333333333333333703, 0.3079598441704289313, 0.3333333333333333703),
 ( 0.3333333333333333703, 0.3079598441704289313, 0.3333333333333333703, 0.3079598441704289313, 0.3333333333333333703, 0.3079598441704289313, 0.3333333333333333703, 0.3079598441704289313, 0.3333333333333333703, 0.3079598441704289313, 0.3333333333333333703, 0.3079598441704289313, 0.3333333333333333703, 0.3079598441704289313, 0.3333333333333333703, 0.3079598441704289313, 0.3333333333333333703, 0.3079598441704289313, 0.3333333333333333703, 0.3079598441704289313, 0.3333333333333333703, 0.3079598441704289313, 0.3333333333333333703, 0.3079598441704289313, 0.3333333333333333703, 0.3079598441704289313, 0.3333333333333333703, 0.3079598441704289313, 0.3333333333333333703, 0.3079598441704289313, 0.3333333333333333703, 0.3079598441704289313, 0.3333333333333333703, 0.3079598441704289313, 0.3333333333333333703, 0.3079598441704289313, 0.3333333333333333703, 0.3079598441704289313, 0.3333333333333333703, 0.3079598441704289313, 0.3333333333333333703, 0.3079598441704289313, 0.3333333333333333703, 0.3079598441704289313, 0.3333333333333333703, 0.3079598441704289313, 0.3333333333333333703, 0.3079598441704289313, 0.3333333333333333703, 0.3079598441704289313, 0.3333333333333333703, 0.3079598441704289313, 0.3333333333333333703, 0.3079598441704289313, 0.3333333333333333703, 0.3079598441704289313, 0.3333333333333333703, 0.3079598441704289313, 0.3333333333333333703, 0.3079598441704289313, 0.3333333333333333703, 0.3079598441704289313, 0.3333333333333333703, 0.3079598441704289313, 0.3333333333333333703, 0.3079598441704289313, 0.3333333333333333703, 0.3079598441704289313, 0.3333333333333333703, 0.3079598441704289313, 0.3333333333333333703, 0.3079598441704289313, 0.3333333333333333703, 0.3079598441704289313, 0.3333333333333333703, 0.3079598441704289313, 0.3333333333333333703, 0.3079598441704289313, 0.3333333333333333703, 0.3079598441704289313, 0.3333333333333333703, 0.3079598441704289313, 0.3333333333333333703, 0.3079598441704289313, 0.3333333333333333703, 0.3079598441704289313, 0.3333333333333333703, 0.3079598441704289313, 0.3333333333333333703, 0.3079598441704289313, 0.3333333333333333703, 0.3079598441704289313, 0.3333333333333333703, 0.3079598441704289313, 0.3333333333333333703, 0.3079598441704289313, 0.3333333333333333703),
 ( 1.000000000000000000, 0.9238795325112867385, 1.000000000000000000, 0.9238795325112867385, 1.000000000000000000, 0.9238795325112867385, 1.000000000000000000, 0.9238795325112867385, 1.000000000000000000, 0.9238795325112867385, 1.000000000000000000, 0.9238795325112867385, 1.000000000000000000, 0.9238795325112867385, 1.000000000000000000, 0.9238795325112867385, 1.000000000000000000, 0.9238795325112867385, 1.000000000000000000, 0.9238795325112867385, 1.000000000000000000, 0.9238795325112867385, 1.000000000000000000, 0.9238795325112867385, 1.000000000000000000, 0.9238795325112867385, 1.000000000000000000, 0.9238795325112867385, 1.000000000000000000, 0.9238795325112867385, 1.000000000000000000, 0.9238795325112867385, 1.000000000000000000, 0.9238795325112867385, 1.000000000000000000, 0.9238795325112867385, 1.000000000000000000, 0.9238795325112867385, 1.000000000000000000, 0.9238795325112867385, 1.000000000000000000, 0.9238795325112867385, 1.000000000000000000, 0.9238795325112867385, 1.000000000000000000, 0.9238795325112867385, 1.000000000000000000, 0.9238795325112867385, 1.000000000000000000, 0.9238795325112867385, 1.000000000000000000, 0.9238795325112867385, 1.000000000000000000, 0.9238795325112867385, 1.000000000000000000, 0.9238795325112867385, 1.000000000000000000, 0.9238795325112867385, 1.000000000000000000, 0.9238795325112867385, 1.000000000000000000, 0.9238795325112867385, 1.000000000000000000, 0.9238795325112867385, 1.000000000000000000, 0.9238795325112867385, 1.000000000000000000, 0.9238795325112867385, 1.000000000000000000, 0.9238795325112867385, 1.000000000000000000, 0.9238795325112867385, 1.000000000000000000, 0.9238795325112867385, 1.000000000000000000, 0.9238795325112867385, 1.000000000000000000, 0.9238795325112867385, 1.000000000000000000, 0.9238795325112867385, 1.000000000000000000, 0.9238795325112867385, 1.000000000000000000, 0.9238795325112867385, 1.000000000000000000, 0.9238795325112867385, 1.000000000000000000, 0.9238795325112867385, 1.000000000000000000, 0.9238795325112867385, 1.000000000000000000, 0.9238795325112867385, 1.000000000000000000, 0.9238795325112867385, 1.000000000000000000, 0.9238795325112867385, 1.000000000000000000) ) ) 
 REPRESENTATION_ITEM ( '' )  SURFACE ( )  );
#3082=CARTESIAN_POINT ( 'NONE',  ( 10.66011273973178852, 1.083605698617464244E-14, -4.403548868934727523 ) ) ;
#3097=CARTESIAN_POINT ( 'NONE',  ( -8.043339635997654113, -77.00624999999982379, 8.043339635996302306 ) ) ;
#3124=CARTESIAN_POINT ( 'NONE',  ( -13.16986379959834252, -30.14374999999995097, -13.16986379960055409 ) ) ;
#3131=CARTESIAN_POINT ( 'NONE',  ( 7.714727599197340524, -89.52812499999977547, 18.62500000000063949 ) ) ;
#3139=CARTESIAN_POINT ( 'NONE',  ( 4.711679271994909435, -69.72187499999982663, -11.37499999999960387 ) ) ;
#3154=CARTESIAN_POINT ( 'NONE',  ( -13.16986379960055409, -100.9062499999997868, 13.16986379959834252 ) ) ;
#3167=CARTESIAN_POINT ( 'NONE',  ( 18.55549153077629398, 8.384379708534148161E-15, -1.770424328178711759 ) ) ;
#3185=CARTESIAN_POINT ( 'NONE',  ( -4.711679271994916540, -4.196874999999971934, 11.37499999999960565 ) ) ;
#3186=CARTESIAN_POINT ( 'NONE',  ( 11.37500000000000000, -83.24999999999980105, 9.531744055041752924E-13 ) ) ;
#3193=CARTESIAN_POINT ( 'NONE',  ( 18.62500000000000000, -16.64999999999995950, 1.560692158462880521E-12 ) ) ;
#3202=MANIFOLD_SOLID_BREP ( 'Cut-Extrude2', #5220 ) ;
#3215=CARTESIAN_POINT ( 'NONE',  ( -18.62500000000000000, -48.87499999999990052, -1.562973063126292757E-12 ) ) ;
#3221=CARTESIAN_POINT ( 'NONE',  ( -11.37499999999960743, -0.03437499999998146899, -4.711679271994912099 ) ) ;
#3230=CARTESIAN_POINT ( 'NONE',  ( -11.37500000000000000, -74.92499999999982663, -9.545674412382054647E-13 ) ) ;
#3243=CARTESIAN_POINT ( 'NONE',  ( -13.16986379959834252, -6.243749999999985256, -13.16986379960055054 ) ) ;
#3245=CARTESIAN_POINT ( 'NONE',  ( -1.564113515457998370E-12, -53.03749999999988773, 18.62500000000000000 ) ) ;
#3276=CARTESIAN_POINT ( 'NONE',  ( 9.538709233711902776E-13, -13.56249999999995026, -11.37500000000000178 ) ) ;
#3277=CARTESIAN_POINT ( 'NONE',  ( -11.37499999999960387, -23.93437499999994245, -4.711679271994911211 ) ) ;
#3283=CARTESIAN_POINT ( 'NONE',  ( -18.62500000000000000, -24.97499999999994102, -1.562973063126292555E-12 ) ) ;
#3306=CARTESIAN_POINT ( 'NONE',  ( -13.16986379960055409, -100.9062499999997868, 13.16986379959834252 ) ) ;
#3315=CARTESIAN_POINT ( 'NONE',  ( 11.37499999999960565, -25.00937499999992397, 4.711679271994918317 ) ) ;
#3323=CARTESIAN_POINT ( 'NONE',  ( 9.538709233711902776E-13, -28.06249999999995381, -11.37499999999999645 ) ) ;
#3340=CARTESIAN_POINT ( 'NONE',  ( 7.714727599197338748, -30.17812499999993747, 18.62500000000063949 ) ) ;
#3343=CARTESIAN_POINT ( 'NONE',  ( 1.561832610794586538E-12, -4.162499999999989875, -18.62500000000000000 ) ) ;
#3358=CARTESIAN_POINT ( 'NONE',  ( 4.711679271993006068, -63.47812499999984226, 11.37500000000039257 ) ) ;
#3369=CARTESIAN_POINT ( 'NONE',  ( 18.62499999999935341, -74.95937499999980957, 7.714727599200469577 ) ) ;
#3370=CARTESIAN_POINT ( 'NONE',  ( -9.552639591052204498E-13, -62.43749999999985079, 11.37500000000000000 ) ) ;
#3374=CARTESIAN_POINT ( 'NONE',  ( 18.62500000000064304, -67.64062499999984368, -7.714727599197334307 ) ) ;
#3392=ORIENTED_EDGE ( 'NONE', *, *, #4542, .F. ) ;
#3395=CARTESIAN_POINT ( 'NONE',  ( 13.16986379960055054, -18.73124999999995666, -13.16986379959834430 ) ) ;
#3404=CARTESIAN_POINT ( 'NONE',  ( -4.711679271993003404, -47.90312499999986784, -11.37500000000039613 ) ) ;
#3412=CARTESIAN_POINT ( 'NONE',  ( -9.552639591052204498E-13, -79.08749999999980673, 11.37500000000000000 ) ) ;
#3426=CARTESIAN_POINT ( 'NONE',  ( 18.62500000000064304, -17.69062499999995453, -7.714727599197335195 ) ) ;
#3428=CARTESIAN_POINT ( 'NONE',  ( -13.16986379960055231, -43.70624999999989768, 13.16986379959834252 ) ) ;
#3445=CARTESIAN_POINT ( 'NONE',  ( -8.043339635997652337, -17.65624999999997513, 8.043339635996300530 ) ) ;
#3456=CARTESIAN_POINT ( 'NONE',  ( 8.043339635997652337, 5.168750000000006395, -8.043339635996304082 ) ) ;
#3457=CARTESIAN_POINT ( 'NONE',  ( 11.37500000000000000, -99.89999999999976410, 0.000000000000000000 ) ) ;
#3461=CARTESIAN_POINT ( 'NONE',  ( 18.62500000000000000, -49.94999999999988205, 1.560692158462880521E-12 ) ) ;
#3462=CARTESIAN_POINT ( 'NONE',  ( 15.00000000000000000, -99.89999999999999147, 0.000000000000000000 ) ) ;
#3480=CARTESIAN_POINT ( 'NONE',  ( -7.714727599200467800, -11.44687499999997371, 18.62499999999934630 ) ) ;
#3487=CARTESIAN_POINT ( 'NONE',  ( 11.06573348676161217, -99.99999999999995737, 3.020779226708963261 ) ) ;
#3489=CARTESIAN_POINT ( 'NONE',  ( -4.711679271993003404, -14.60312499999994706, -11.37500000000039613 ) ) ;
#3496=CARTESIAN_POINT ( 'NONE',  ( -4.711679271993004292, -88.45312499999978684, -11.37500000000039435 ) ) ;
#3506=CARTESIAN_POINT ( 'NONE',  ( -1.564113515457998572E-12, -62.43749999999985079, 18.62500000000000000 ) ) ;
#3508=CARTESIAN_POINT ( 'NONE',  ( -1.564113515457998572E-12, -62.43749999999985079, 18.62500000000000000 ) ) ;
#3510=CARTESIAN_POINT ( 'NONE',  ( 18.62499999999934630, -15.60937499999996270, 7.714727599200467800 ) ) ;
#3527=CARTESIAN_POINT ( 'NONE',  ( -9.552639591052204498E-13, -36.38749999999993179, 11.37499999999999645 ) ) ;
#3536=CARTESIAN_POINT ( 'NONE',  ( 8.043339635996302306, -7.318749999999964118, 8.043339635997654113 ) ) ;
#3542=CARTESIAN_POINT ( 'NONE',  ( -7.714727599197334307, -88.45312499999977263, -18.62500000000064304 ) ) ;
#3564=CARTESIAN_POINT ( 'NONE',  ( 1.561832610794586538E-12, -4.162499999999989875, -18.62500000000000000 ) ) ;
#3574=CARTESIAN_POINT ( 'NONE',  ( 8.043339635996302306, -57.26874999999984794, 8.043339635997654113 ) ) ;
#3580=CARTESIAN_POINT ( 'NONE',  ( 9.538709233711902776E-13, -44.71249999999991331, -11.37499999999999645 ) ) ;
#3586=CARTESIAN_POINT ( 'NONE',  ( 0.000000000000000000, -100.0000000000000000, 0.000000000000000000 ) ) ;
#3591=CARTESIAN_POINT ( 'NONE',  ( -18.62499999999934985, -57.23437499999987921, -7.714727599200458918 ) ) ;
#3593=CARTESIAN_POINT ( 'NONE',  ( -18.62499999999934985, -23.93437499999993889, -7.714727599200458918 ) ) ;
#3595=CARTESIAN_POINT ( 'NONE',  ( -13.16986379960055231, -60.35624999999985363, 13.16986379959834252 ) ) ;
#3614=CARTESIAN_POINT ( 'NONE',  ( 4.711679271994911211, -60.32187499999988489, -11.37499999999960210 ) ) ;
#3623=CARTESIAN_POINT ( 'NONE',  ( 11.37500000000039435, -1.040624999999997025, -4.711679271993004292 ) ) ;
#3624=CARTESIAN_POINT ( 'NONE',  ( -4.711679271993003404, -88.45312499999977263, -11.37500000000039435 ) ) ;
#3630=CARTESIAN_POINT ( 'NONE',  ( 1.561832610794586538E-12, -70.76249999999983231, -18.62500000000000000 ) ) ;
#3656=CARTESIAN_POINT ( 'NONE',  ( -18.62499999999934985, -7.284374999999982947, -7.714727599200458918 ) ) ;
#3664=CARTESIAN_POINT ( 'NONE',  ( 8.318912088914551362, -99.99999999999994316, 8.890191110864586577 ) ) ;
#3666=CARTESIAN_POINT ( 'NONE',  ( -11.37499999999960743, -49.98437499999987210, -4.711679271994912099 ) ) ;
#3674=CARTESIAN_POINT ( 'NONE',  ( -4.711679271994916540, -94.69687499999979252, 11.37499999999960210 ) ) ;
#3683=CARTESIAN_POINT ( 'NONE',  ( -7.714727599197335195, -55.15312499999986784, -18.62500000000064304 ) ) ;
#3686=CARTESIAN_POINT ( 'NONE',  ( -18.62499999999934985, -73.88437499999982094, -7.714727599200458918 ) ) ;
#3689=CARTESIAN_POINT ( 'NONE',  ( 13.16986379959834075, -47.86874999999988489, 13.16986379960055231 ) ) ;
#3705=CARTESIAN_POINT ( 'NONE',  ( 9.538709233711902776E-13, -28.06249999999995381, -11.37499999999999645 ) ) ;
#3714=CARTESIAN_POINT ( 'NONE',  ( 4.711679271994911211, -62.47187499999984084, -11.37499999999960743 ) ) ;
#3743=CARTESIAN_POINT ( 'NONE',  ( 13.16986379959834075, -64.51874999999984084, 13.16986379960055231 ) ) ;
#3752=CARTESIAN_POINT ( 'NONE',  ( 5.348135253449231463, -100.0000000000000000, 12.08639588262338016 ) ) ;
#3754=CARTESIAN_POINT ( 'NONE',  ( -8.043339635996302306, -6.243749999999984368, -8.043339635997654113 ) ) ;
#3765=CARTESIAN_POINT ( 'NONE',  ( 11.37499999999999645, -57.19999999999988916, 9.531744055041752924E-13 ) ) ;
#3772=CARTESIAN_POINT ( 'NONE',  ( 13.16986379960055054, -68.68124999999983515, -13.16986379959834430 ) ) ;
#3774=CARTESIAN_POINT ( 'NONE',  ( 18.62500000000000000, -83.24999999999980105, 1.560692158462880521E-12 ) ) ;
#3777=CARTESIAN_POINT ( 'NONE',  ( -1.564113515457998572E-12, -62.43749999999985079, 18.62500000000000000 ) ) ;
#3795=CARTESIAN_POINT ( 'NONE',  ( -4.711679271993001628, -45.75312499999991189, -11.37500000000039613 ) ) ;
#3806=CARTESIAN_POINT ( 'NONE',  ( 11.37500000000000000, 4.439344646909156023E-16, 9.531744055041752924E-13 ) ) ;
#3824=ORIENTED_EDGE ( 'NONE', *, *, #4756, .T. ) ;
#3831=CARTESIAN_POINT ( 'NONE',  ( 1.561832610794586538E-12, -70.76249999999983231, -18.62500000000000000 ) ) ;
#3839=CARTESIAN_POINT ( 'NONE',  ( 4.711679271993006068, -30.17812499999993747, 11.37500000000039257 ) ) ;
#3848=CARTESIAN_POINT ( 'NONE',  ( -11.37499999999960210, -64.48437499999987210, -4.711679271994911211 ) ) ;
#3856=CARTESIAN_POINT ( 'NONE',  ( -18.62500000000064659, -59.31562499999985505, 7.714727599197335195 ) ) ;
#3858=CARTESIAN_POINT ( 'NONE',  ( -18.62500000000000000, -1.074999999999978639, -1.562973063126292757E-12 ) ) ;
#3861=CARTESIAN_POINT ( 'NONE',  ( -7.714727599200467800, -78.04687499999982947, 18.62499999999934630 ) ) ;
#3873=PRODUCT_CONTEXT ( 'NONE', #17138, 'mechanical' ) ;
#3878=CARTESIAN_POINT ( 'NONE',  ( -11.37500000000039613, -99.86562499999978115, 4.711679271993000739 ) ) ;
#3887=CARTESIAN_POINT ( 'NONE',  ( 8.043339635996302306, -40.61874999999988489, 8.043339635997654113 ) ) ;
#3888=CARTESIAN_POINT ( 'NONE',  ( -13.16986379959834252, -6.243749999999985256, -13.16986379960055054 ) ) ;
#3892=CARTESIAN_POINT ( 'NONE',  ( 18.62500000000000000, -99.89999999999976410, 0.000000000000000000 ) ) ;
#3914=CARTESIAN_POINT ( 'NONE',  ( -1.564113515457998572E-12, -95.73749999999976978, 18.62500000000000000 ) ) ;
#3926=CARTESIAN_POINT ( 'NONE',  ( 4.711679271994911211, -79.12187499999980389, -11.37499999999960743 ) ) ;
#3935=CARTESIAN_POINT ( 'NONE',  ( 8.043339635996298753, -55.11874999999988489, 8.043339635997652337 ) ) ;
#3939=PRODUCT_DEFINITION ( 'UNKNOWN', '', #6528, #10736 ) ;
#3942=CARTESIAN_POINT ( 'NONE',  ( 7.714727599200456254, -12.52187499999995524, -18.62499999999935341 ) ) ;
#3944=CARTESIAN_POINT ( 'NONE',  ( -18.62500000000064659, -92.61562499999978115, 7.714727599197335195 ) ) ;
#3948=CARTESIAN_POINT ( 'NONE',  ( 18.62500000000000000, -99.89999999999976410, 1.560692158462880521E-12 ) ) ;
#3968=CARTESIAN_POINT ( 'NONE',  ( -18.62499999999935341, -14.53437499999998650, -7.714727599200458030 ) ) ;
#3976=CARTESIAN_POINT ( 'NONE',  ( -11.37500000000000178, -67.67499999999981242, -9.545674412382054647E-13 ) ) ;
#3977=CARTESIAN_POINT ( 'NONE',  ( 7.714727599200458030, -36.42187499999990763, -18.62499999999934985 ) ) ;
#4000=CARTESIAN_POINT ( 'NONE',  ( -18.62500000000000000, -41.62499999999990052, -1.562973063126292555E-12 ) ) ;
#4014=CARTESIAN_POINT ( 'NONE',  ( 8.043339635996300530, -31.21874999999992539, 8.043339635997654113 ) ) ;
#4023=CARTESIAN_POINT ( 'NONE',  ( 4.711679271993006957, -70.72812499999983515, 11.37500000000039257 ) ) ;
#4029=CARTESIAN_POINT ( 'NONE',  ( -18.62499999999935341, -16.68437499999993889, -7.714727599200458030 ) ) ;
#4031=CARTESIAN_POINT ( 'NONE',  ( -18.62499999999935341, -0.03437499999998146899, -7.714727599200458030 ) ) ;
#4034=CARTESIAN_POINT ( 'NONE',  ( -13.16986379960055231, -93.65624999999977263, 13.16986379959834252 ) ) ;
#4037=EDGE_LOOP ( 'NONE', ( #1893, #5555 ) ) ;
#4052=CARTESIAN_POINT ( 'NONE',  ( -1.564113515457998370E-12, -19.73749999999997229, 18.62500000000000000 ) ) ;
#4060=CARTESIAN_POINT ( 'NONE',  ( 11.37500000000000000, -49.94999999999988205, 9.531744055041752924E-13 ) ) ;
#4061=CARTESIAN_POINT ( 'NONE',  ( -18.62500000000064659, -26.01562499999994671, 7.714727599197335195 ) ) ;
#4067=EDGE_CURVE ( 'NONE', #7126, #16308, #16542, .T. ) ;
#4082=CARTESIAN_POINT ( 'NONE',  ( 4.711679271993006068, -13.52812499999996909, 11.37500000000039257 ) ) ;
#4086=CARTESIAN_POINT ( 'NONE',  ( -18.62500000000064659, -42.66562499999989200, 7.714727599197335195 ) ) ;
#4100=CARTESIAN_POINT ( 'NONE',  ( 4.711679271994909435, -3.121874999999992184, -11.37499999999960387 ) ) ;
#4111=CARTESIAN_POINT ( 'NONE',  ( 11.37499999999999645, -73.84999999999983800, 9.531744055041752924E-13 ) ) ;
#4118=CARTESIAN_POINT ( 'NONE',  ( 1.561832610794586740E-12, -13.56249999999995026, -18.62500000000000000 ) ) ;
#4120=CARTESIAN_POINT ( 'NONE',  ( 13.16986379960055054, -85.33124999999978400, -13.16986379959834430 ) ) ;
#4141=CARTESIAN_POINT ( 'NONE',  ( 18.62500000000064659, -8.290625000000000355, -7.714727599197336083 ) ) ;
#4151=CARTESIAN_POINT ( 'NONE',  ( 7.714727599197338748, -13.52812499999996732, 18.62500000000063949 ) ) ;
#4156=CARTESIAN_POINT ( 'NONE',  ( 4.905322627110114908, 5.715075095792292317E-16, -15.60939936909243819 ) ) ;
#4180=CARTESIAN_POINT ( 'NONE',  ( 7.714727599200458030, -19.77187499999995168, -18.62499999999935341 ) ) ;
#4188=CARTESIAN_POINT ( 'NONE',  ( 3.604077478036761484, -100.0000000000000142, 14.28339603699808258 ) ) ;
#4191=CARTESIAN_POINT ( 'NONE',  ( 8.043339635996300530, -64.51874999999984084, 8.043339635997654113 ) ) ;
#4202=CARTESIAN_POINT ( 'NONE',  ( 18.62499999999935341, -22.85937499999996803, 7.714727599200469577 ) ) ;
#4207=CARTESIAN_POINT ( 'NONE',  ( 18.62500000000064659, -43.74062499999988773, -7.714727599197336083 ) ) ;
#4209=CARTESIAN_POINT ( 'NONE',  ( 18.62500000000064659, -77.04062499999979252, -7.714727599197336083 ) ) ;
#4233=CARTESIAN_POINT ( 'NONE',  ( -7.714727599197334307, -45.75312499999991189, -18.62500000000064659 ) ) ;
#4246=CARTESIAN_POINT ( 'NONE',  ( 3.814188548975826709, -6.916538280674965647E-15, -13.28211646800023082 ) ) ;
#4280=CARTESIAN_POINT ( 'NONE',  ( -11.37499999999960387, -73.88437499999982094, -4.711679271994910323 ) ) ;
#4290=CARTESIAN_POINT ( 'NONE',  ( 7.714727599200456254, -60.32187499999988489, -18.62499999999935341 ) ) ;
#4295=CARTESIAN_POINT ( 'NONE',  ( 18.62499999999935341, -8.359374999999960920, 7.714727599200469577 ) ) ;
#4297=CARTESIAN_POINT ( 'NONE',  ( 13.16986379959833897, -40.61874999999988489, 13.16986379960055409 ) ) ;
#4320=CARTESIAN_POINT ( 'NONE',  ( 13.16986379960055409, -59.28124999999987921, -13.16986379959834430 ) ) ;
#4322=SHAPE_REPRESENTATION ( 'Spring', ( #16654 ), #7660 ) ;
#4334=CARTESIAN_POINT ( 'NONE',  ( 7.799367850303418948, -7.609836600491641030E-16, -9.406362677511159731 ) ) ;
#4335=DIRECTION ( 'NONE',  ( 0.000000000000000000, 0.000000000000000000, 1.000000000000000000 ) ) ;
#4350=CARTESIAN_POINT ( 'NONE',  ( -11.37500000000039613, -42.66562499999989200, 4.711679271993001628 ) ) ;
#4369=CARTESIAN_POINT ( 'NONE',  ( -4.711679271994916540, -44.74687499999989626, 11.37499999999960210 ) ) ;
#4380=CARTESIAN_POINT ( 'NONE',  ( 13.16986379959833897, -71.76874999999985505, 13.16986379960055409 ) ) ;
#4386=CARTESIAN_POINT ( 'NONE',  ( 18.62500000000000000, -59.34999999999983800, 1.560692158462880521E-12 ) ) ;
#4393=CARTESIAN_POINT ( 'NONE',  ( 11.37500000000039435, -34.34062499999991047, -4.711679271993004292 ) ) ;
#4410=FACE_OUTER_BOUND ( 'NONE', #2452, .T. ) ;
#4412=CARTESIAN_POINT ( 'NONE',  ( 7.714727599197340524, -87.37812499999982663, 18.62500000000063949 ) ) ;
#4426=CARTESIAN_POINT ( 'NONE',  ( 4.464927919665403699, 5.715075095792275554E-16, -15.55360924457959371 ) ) ;
#4443=CARTESIAN_POINT ( 'NONE',  ( 8.043339635996300530, -64.51874999999984084, 8.043339635997654113 ) ) ;
#4450=CARTESIAN_POINT ( 'NONE',  ( -13.16986379959834252, -6.243749999999985256, -13.16986379960055054 ) ) ;
#4462=CARTESIAN_POINT ( 'NONE',  ( 11.37500000000000000, -99.89999999999976410, 9.531744055041752924E-13 ) ) ;
#4472=CARTESIAN_POINT ( 'NONE',  ( 18.62500000000064659, -58.24062499999988063, -7.714727599197336083 ) ) ;
#4479=CARTESIAN_POINT ( 'NONE',  ( -18.62500000000000000, -67.67499999999981242, -1.562973063126292757E-12 ) ) ;
#4484=CARTESIAN_POINT ( 'NONE',  ( -8.043339635997654113, -10.40624999999997513, 8.043339635996302306 ) ) ;
#4502=CARTESIAN_POINT ( 'NONE',  ( -18.62499999999935341, -81.13437499999982094, -7.714727599200458030 ) ) ;
#4513=CARTESIAN_POINT ( 'NONE',  ( 18.62500000000000000, 0.000000000000000000, 1.560692158462880521E-12 ) ) ;
#4528=CARTESIAN_POINT ( 'NONE',  ( -7.714727599200466912, -87.44687499999976410, 18.62499999999935341 ) ) ;
#4529=CARTESIAN_POINT ( 'NONE',  ( 8.043339635996300530, -81.16874999999980389, 8.043339635997654113 ) ) ;
#4535=CARTESIAN_POINT ( 'NONE',  ( 13.16986379960055054, -2.081249999999994937, -13.16986379959834430 ) ) ;
#4542=EDGE_CURVE ( 'NONE', #9435, #7272, #5284, .T. ) ;
#4557=CARTESIAN_POINT ( 'NONE',  ( -1.564113515457998370E-12, -36.38749999999993179, 18.62500000000000000 ) ) ;
#4564=CARTESIAN_POINT ( 'NONE',  ( -8.043339635996304082, 1.006250000000015854, -8.043339635997652337 ) ) ;
#4572=CARTESIAN_POINT ( 'NONE',  ( -4.711679271993004292, -71.80312499999982379, -11.37500000000039435 ) ) ;
#4589=CARTESIAN_POINT ( 'NONE',  ( -7.714727599200466912, -68.64687499999988063, 18.62499999999935341 ) ) ;
#4615=CARTESIAN_POINT ( 'NONE',  ( -9.552639591052204498E-13, -5.237499999999969624, 11.37500000000000178 ) ) ;
#4616=CARTESIAN_POINT ( 'NONE',  ( 4.711679271994910323, -86.37187499999978968, -11.37499999999960387 ) ) ;
#4622=CARTESIAN_POINT ( 'NONE',  ( -13.16986379959834252, -39.54374999999990337, -13.16986379960055054 ) ) ;
#4643=CARTESIAN_POINT ( 'NONE',  ( 7.714727599200456254, -93.62187499999978968, -18.62499999999935341 ) ) ;
#4651=CARTESIAN_POINT ( 'NONE',  ( -11.37499999999960743, -33.33437499999990195, -4.711679271994912099 ) ) ;
#4659=CARTESIAN_POINT ( 'NONE',  ( -4.711679271993004292, -38.50312499999991189, -11.37500000000039435 ) ) ;
#4675=CARTESIAN_POINT ( 'NONE',  ( 18.62500000000064304, -34.34062499999991047, -7.714727599197335195 ) ) ;
#4677=CARTESIAN_POINT ( 'NONE',  ( -1.564113515457998370E-12, -102.9874999999997698, 18.62500000000000000 ) ) ;
#4702=CARTESIAN_POINT ( 'NONE',  ( -11.37500000000039790, -35.41562499999989200, 4.711679271993001628 ) ) ;
#4703=CARTESIAN_POINT ( 'NONE',  ( -4.711679271993003404, -21.85312499999994884, -11.37500000000039435 ) ) ;
#4708=CARTESIAN_POINT ( 'NONE',  ( -13.16986379960055231, -60.35624999999985363, 13.16986379959834252 ) ) ;
#4730=CARTESIAN_POINT ( 'NONE',  ( -18.62499999999935341, -97.78437499999979821, -7.714727599200458030 ) ) ;
#4737=CARTESIAN_POINT ( 'NONE',  ( -4.711679271994916540, -4.196874999999971934, 11.37499999999960565 ) ) ;
#4745=CARTESIAN_POINT ( 'NONE',  ( -4.711679271994915652, -18.69687499999997726, 11.37499999999960210 ) ) ;
#4756=EDGE_CURVE ( 'NONE', #9435, #16308, #2934, .T. ) ;
#4760=CARTESIAN_POINT ( 'NONE',  ( 13.16986379959834075, -14.56874999999996589, 13.16986379960055231 ) ) ;
#4763=CARTESIAN_POINT ( 'NONE',  ( 1.561832610794586538E-12, -37.46249999999991331, -18.62500000000000000 ) ) ;
#4780=CARTESIAN_POINT ( 'NONE',  ( 4.711679271994909435, -86.37187499999978968, -11.37499999999960387 ) ) ;
#4790=CARTESIAN_POINT ( 'NONE',  ( 11.37500000000000178, -26.04999999999992255, 9.531744055041752924E-13 ) ) ;
#4795=CARTESIAN_POINT ( 'NONE',  ( -7.714727599197334307, -38.50312499999991189, -18.62500000000064304 ) ) ;
#4814=CARTESIAN_POINT ( 'NONE',  ( -7.714727599200467800, -28.09687499999992966, 18.62499999999934630 ) ) ;
#4823=CARTESIAN_POINT ( 'NONE',  ( -4.711679271993003404, -31.25312499999991545, -11.37500000000039613 ) ) ;
#4830=CARTESIAN_POINT ( 'NONE',  ( -11.37499999999999645, -32.22499999999993747, -9.545674412382054647E-13 ) ) ;
#4841=CARTESIAN_POINT ( 'NONE',  ( 1.561832610794586538E-12, -54.11249999999986926, -18.62500000000000000 ) ) ;
#4843=CARTESIAN_POINT ( 'NONE',  ( -7.714727599200467800, -61.39687499999984510, 18.62499999999934630 ) ) ;
#4845=CARTESIAN_POINT ( 'NONE',  ( -18.62500000000000000, -8.324999999999979750, -1.562973063126292555E-12 ) ) ;
#4864=CARTESIAN_POINT ( 'NONE',  ( 11.37499999999960210, -22.85937499999996092, 4.711679271994916540 ) ) ;
#4874=CARTESIAN_POINT ( 'NONE',  ( 7.714727599197340524, -72.87812499999979821, 18.62500000000063949 ) ) ;
#4879=CARTESIAN_POINT ( 'NONE',  ( 18.62500000000064304, -50.99062499999988063, -7.714727599197334307 ) ) ;
#4902=CARTESIAN_POINT ( 'NONE',  ( 18.62500000000064659, -91.54062499999980673, -7.714727599197336083 ) ) ;
#4913=CARTESIAN_POINT ( 'NONE',  ( 11.37499999999960565, -8.359374999999960920, 4.711679271994918317 ) ) ;
#4920=CARTESIAN_POINT ( 'NONE',  ( 9.538709233711902776E-13, -87.41249999999979536, -11.37500000000000000 ) ) ;
#4929=CARTESIAN_POINT ( 'NONE',  ( 7.714727599197338748, -80.12812499999981242, 18.62500000000063949 ) ) ;
#4931=CARTESIAN_POINT ( 'NONE',  ( 7.714727599200458030, -69.72187499999982663, -18.62499999999934985 ) ) ;
#4934=CARTESIAN_POINT ( 'NONE',  ( -7.714727599197335195, -55.15312499999986784, -18.62500000000064304 ) ) ;
#4953=CARTESIAN_POINT ( 'NONE',  ( -4.711679271994915652, -68.64687499999988063, 11.37499999999960210 ) ) ;
#4962=CARTESIAN_POINT ( 'NONE',  ( -11.37500000000039613, -9.365624999999976552, 4.711679271993002516 ) ) ;
#4963=CARTESIAN_POINT ( 'NONE',  ( -8.043339635997654113, -93.65624999999977263, 8.043339635996302306 ) ) ;
#4965=CARTESIAN_POINT ( 'NONE',  ( 13.16986379960055054, -52.03124999999987921, -13.16986379959834430 ) ) ;
#4989=CARTESIAN_POINT ( 'NONE',  ( -18.62500000000000000, -82.17499999999982663, -1.562973063126292757E-12 ) ) ;
#5000=CARTESIAN_POINT ( 'NONE',  ( 9.538709233711902776E-13, -30.21249999999990976, -11.37500000000000178 ) ) ;
#5008=CARTESIAN_POINT ( 'NONE',  ( -8.043339635996300530, -46.79374999999990337, -8.043339635997652337 ) ) ;
#5016=CARTESIAN_POINT ( 'NONE',  ( -18.62499999999935341, -0.03437499999998146899, -7.714727599200458030 ) ) ;
#5018=CARTESIAN_POINT ( 'NONE',  ( 1.561832610794586538E-12, -70.76249999999983231, -18.62500000000000000 ) ) ;
#5021=CARTESIAN_POINT ( 'NONE',  ( -18.62500000000064659, -26.01562499999994671, 7.714727599197335195 ) ) ;
#5038=SHAPE_DEFINITION_REPRESENTATION ( #8202, #4322 ) ;
#5044=CARTESIAN_POINT ( 'NONE',  ( 9.538709233711902776E-13, -78.01249999999981810, -11.37499999999999645 ) ) ;
#5053=CARTESIAN_POINT ( 'NONE',  ( -8.043339635996304082, -65.59374999999981526, -8.043339635997652337 ) ) ;
#5081=ORIENTED_EDGE ( 'NONE', *, *, #17355, .F. ) ;
#5083=CARTESIAN_POINT ( 'NONE',  ( 18.62500000000000000, -99.89999999999976410, 1.560692158462880521E-12 ) ) ;
#5092=CARTESIAN_POINT ( 'NONE',  ( 10.96735208155292973, -99.99999999999997158, 3.443427092386485366 ) ) ;
#5094=CARTESIAN_POINT ( 'NONE',  ( -9.552639591052204498E-13, -88.48749999999975557, 11.37500000000000178 ) ) ;
#5103=CARTESIAN_POINT ( 'NONE',  ( 8.043339635997652337, -92.58124999999978400, -8.043339635996302306 ) ) ;
#5110=CARTESIAN_POINT ( 'NONE',  ( 7.714727599200458030, -53.07187499999987068, -18.62499999999934985 ) ) ;
#5112=CARTESIAN_POINT ( 'NONE',  ( 7.714727599200456254, -29.17187499999991118, -18.62499999999935341 ) ) ;
#5115=CARTESIAN_POINT ( 'NONE',  ( 7.714727599197338748, -13.52812499999996732, 18.62500000000063949 ) ) ;
#5124=FACE_OUTER_BOUND ( 'NONE', #12172, .T. ) ;
#5133=CARTESIAN_POINT ( 'NONE',  ( -8.043339635996300530, -80.09374999999982947, -8.043339635997652337 ) ) ;
#5143=CARTESIAN_POINT ( 'NONE',  ( 11.37500000000039613, -43.74062499999988773, -4.711679271993004292 ) ) ;
#5144=CARTESIAN_POINT ( 'NONE',  ( -8.043339635996302306, -89.49374999999979252, -8.043339635997654113 ) ) ;
#5171=CARTESIAN_POINT ( 'NONE',  ( -13.16986379960055231, -60.35624999999985363, 13.16986379959834252 ) ) ;
#5178=CARTESIAN_POINT ( 'NONE',  ( 4.418379050281270537, -99.99999999999997158, 13.00880126231396439 ) ) ;
#5180=CARTESIAN_POINT ( 'NONE',  ( -4.711679271993004292, -5.203124999999986677, -11.37500000000039435 ) ) ;
#5192=CARTESIAN_POINT ( 'NONE',  ( -13.16986379959834252, -13.49374999999998792, -13.16986379960055409 ) ) ;
#5198=CARTESIAN_POINT ( 'NONE',  ( -13.16986379959834252, -89.49374999999979252, -13.16986379960055054 ) ) ;
#5200=CARTESIAN_POINT ( 'NONE',  ( -1.564113515457998370E-12, -5.237499999999969624, 18.62500000000000000 ) ) ;
#5220=CLOSED_SHELL ( 'NONE', ( #8223, #7461, #11223, #13969, #11929, #11977 ) ) ;
#5222=CARTESIAN_POINT ( 'NONE',  ( 18.62499999999935341, -39.50937499999993463, 7.714727599200469577 ) ) ;
#5232=CARTESIAN_POINT ( 'NONE',  ( 11.37500000000000178, -42.69999999999988205, 9.531744055041752924E-13 ) ) ;
#5233=CARTESIAN_POINT ( 'NONE',  ( -18.62500000000064659, -9.365624999999976552, 7.714727599197335195 ) ) ;
#5258=CARTESIAN_POINT ( 'NONE',  ( 7.714727599197338748, -96.77812499999976126, 18.62500000000063949 ) ) ;
#5269=CARTESIAN_POINT ( 'NONE',  ( 3.808133373400502286, -99.99999999999998579, 14.89041237177510801 ) ) ;
#5271=CARTESIAN_POINT ( 'NONE',  ( 9.538709233711902776E-13, -4.162499999999988987, -11.37500000000000000 ) ) ;
#5272=( GEOMETRIC_REPRESENTATION_CONTEXT ( 3 ) GLOBAL_UNCERTAINTY_ASSIGNED_CONTEXT ( ( #14034 ) ) GLOBAL_UNIT_ASSIGNED_CONTEXT ( ( #8623, #1953, #16898 ) ) REPRESENTATION_CONTEXT ( 'NONE', 'WORKASPACE' ) );
#5281=CARTESIAN_POINT ( 'NONE',  ( 4.711679271993006957, -104.0281249999997755, 11.37500000000039257 ) ) ;
#5284=CIRCLE ( 'NONE', #16556, 3.624999999999999556 ) ;
#5288=CARTESIAN_POINT ( 'NONE',  ( 1.561832610794586740E-12, -46.86249999999987637, -18.62500000000000000 ) ) ;
#5290=CARTESIAN_POINT ( 'NONE',  ( 18.62499999999935341, -8.359374999999960920, 7.714727599200469577 ) ) ;
#5293=CARTESIAN_POINT ( 'NONE',  ( 13.16986379959834075, -81.16874999999980389, 13.16986379960055231 ) ) ;
#5311=CARTESIAN_POINT ( 'NONE',  ( -18.62500000000064659, -16.61562499999998010, 7.714727599197333419 ) ) ;
#5318=CARTESIAN_POINT ( 'NONE',  ( -11.37499999999960743, -49.98437499999987210, -4.711679271994912099 ) ) ;
#5319=CARTESIAN_POINT ( 'NONE',  ( 13.16986379960055054, -35.38124999999991616, -13.16986379959834430 ) ) ;
#5323=CARTESIAN_POINT ( 'NONE',  ( -7.714727599200466912, -94.69687499999976410, 18.62499999999934985 ) ) ;
#5342=CARTESIAN_POINT ( 'NONE',  ( -1.564113515457998572E-12, -45.78749999999988773, 18.62500000000000000 ) ) ;
#5351=CARTESIAN_POINT ( 'NONE',  ( 16.01092576086922747, -100.0000000000000000, 8.948334985424596155 ) ) ;
#5353=CARTESIAN_POINT ( 'NONE',  ( -11.37499999999960387, -7.284374999999982059, -4.711679271994910323 ) ) ;
#5357=ORIENTED_EDGE ( 'NONE', *, *, #10854, .F. ) ;
#5361=ORIENTED_EDGE ( 'NONE', *, *, #12372, .F. ) ;
#5362=CARTESIAN_POINT ( 'NONE',  ( -9.552639591052204498E-13, -102.9874999999997698, 11.37499999999999645 ) ) ;
#5368=CARTESIAN_POINT ( 'NONE',  ( 13.16986379960055409, -28.13124999999991260, -13.16986379959834430 ) ) ;
#5370=CARTESIAN_POINT ( 'NONE',  ( 7.714727599200458030, -86.37187499999978968, -18.62499999999934985 ) ) ;
#5373=CARTESIAN_POINT ( 'NONE',  ( -1.564113515457998572E-12, -79.08749999999980673, 18.62500000000000000 ) ) ;
#5393=CARTESIAN_POINT ( 'NONE',  ( -7.714727599200466912, -35.34687499999993321, 18.62499999999935341 ) ) ;
#5402=CARTESIAN_POINT ( 'NONE',  ( -11.37499999999960387, -40.58437499999990905, -4.711679271994910323 ) ) ;
#5403=CARTESIAN_POINT ( 'NONE',  ( 1.561832610794586538E-12, -20.81249999999995026, -18.62500000000000000 ) ) ;
#5421=CARTESIAN_POINT ( 'NONE',  ( 11.37500000000000000, -9.629649721936179265E-32, 9.531744055041752924E-13 ) ) ;
#5424=CARTESIAN_POINT ( 'NONE',  ( 18.62500000000064304, -84.29062499999983515, -7.714727599197335195 ) ) ;
#5439=CARTESIAN_POINT ( 'NONE',  ( -11.37500000000039790, -85.36562499999978115, 4.711679271993001628 ) ) ;
#5450=CARTESIAN_POINT ( 'NONE',  ( 4.711679271994911211, -93.62187499999978968, -11.37499999999960210 ) ) ;
#5457=CARTESIAN_POINT ( 'NONE',  ( -13.16986379960055409, -53.10624999999986073, 13.16986379959834252 ) ) ;
#5459=CARTESIAN_POINT ( 'NONE',  ( 1.561832610794586740E-12, -13.56249999999995026, -18.62500000000000000 ) ) ;
#5482=CARTESIAN_POINT ( 'NONE',  ( 7.714727599197340524, -20.77812499999997087, 18.62500000000063949 ) ) ;
#5492=CARTESIAN_POINT ( 'NONE',  ( -11.37499999999960387, -57.23437499999987921, -4.711679271994910323 ) ) ;
#5498=CARTESIAN_POINT ( 'NONE',  ( 14.25373764215627226, 2.881527793022514356E-15, -11.25789203224866064 ) ) ;
#5529=CARTESIAN_POINT ( 'NONE',  ( 17.03726630776091611, -100.0000000000000142, 7.069965795335503955 ) ) ;
#5531=CARTESIAN_POINT ( 'NONE',  ( -11.37500000000039613, -92.61562499999978115, 4.711679271993002516 ) ) ;
#5542=CARTESIAN_POINT ( 'NONE',  ( 18.62500000000064659, -41.59062499999991758, -7.714727599197336083 ) ) ;
#5550=CARTESIAN_POINT ( 'NONE',  ( -13.16986379959834252, -15.64374999999994387, -13.16986379960055409 ) ) ;
#5552=CARTESIAN_POINT ( 'NONE',  ( -18.62500000000000000, -84.32499999999977547, -1.562973063126292757E-12 ) ) ;
#5555=ORIENTED_EDGE ( 'NONE', *, *, #8842, .F. ) ;
#5576=CARTESIAN_POINT ( 'NONE',  ( 1.561832610794586740E-12, -44.71249999999991331, -18.62500000000000000 ) ) ;
#5583=DIRECTION ( 'NONE',  ( 1.000000000000000000, 0.000000000000000000, 8.379555213223522577E-14 ) ) ;
#5591=CARTESIAN_POINT ( 'NONE',  ( 17.66377679222614105, 1.677322744816953610E-15, -5.628563848745853804 ) ) ;
#5604=CARTESIAN_POINT ( 'NONE',  ( 8.043339635997654113, -18.73124999999995666, -8.043339635996304082 ) ) ;
#5620=CARTESIAN_POINT ( 'NONE',  ( 4.371733802976720540, -100.0000000000000000, 15.22508764378929058 ) ) ;
#5623=CARTESIAN_POINT ( 'NONE',  ( 11.37500000000000000, -83.24999999999980105, 9.531744055041752924E-13 ) ) ;
#5632=CARTESIAN_POINT ( 'NONE',  ( -7.714727599197334307, -62.40312499999986073, -18.62500000000064659 ) ) ;
#5639=CARTESIAN_POINT ( 'NONE',  ( -13.16986379960055409, -19.80624999999993463, 13.16986379959834252 ) ) ;
#5641=CARTESIAN_POINT ( 'NONE',  ( -1.564113515457998370E-12, -71.83749999999979252, 18.62500000000000000 ) ) ;
#5666=CARTESIAN_POINT ( 'NONE',  ( -13.16986379959834252, -46.79374999999990337, -13.16986379960055409 ) ) ;
#5678=CARTESIAN_POINT ( 'NONE',  ( 3.972737467449376503, -1.623771540364909428E-16, -13.12643016014658848 ) ) ;
#5694=CARTESIAN_POINT ( 'NONE',  ( 8.043339635996300530, -47.86874999999988489, 8.043339635997654113 ) ) ;
#5711=CARTESIAN_POINT ( 'NONE',  ( -9.552639591052204498E-13, -79.08749999999980673, 11.37500000000000000 ) ) ;
#5719=CARTESIAN_POINT ( 'NONE',  ( 18.62500000000000000, -40.54999999999992610, 1.560692158462880521E-12 ) ) ;
#5727=CARTESIAN_POINT ( 'NONE',  ( -13.16986379960055409, -36.45624999999989768, 13.16986379959834252 ) ) ;
#5750=CARTESIAN_POINT ( 'NONE',  ( -18.62500000000000000, -82.17499999999982663, -1.562973063126292757E-12 ) ) ;
#5761=CARTESIAN_POINT ( 'NONE',  ( 9.608090060877380267, -7.486575357575243633E-16, -6.851496304736921061 ) ) ;
#5776=CARTESIAN_POINT ( 'NONE',  ( -11.37500000000000000, -74.92499999999982663, -9.545674412382054647E-13 ) ) ;
#5796=CARTESIAN_POINT ( 'NONE',  ( -9.552639591052204498E-13, -95.73749999999976978, 11.37500000000000000 ) ) ;
#5805=CARTESIAN_POINT ( 'NONE',  ( 7.714727599200456254, -76.97187499999985505, -18.62499999999935341 ) ) ;
#5814=CARTESIAN_POINT ( 'NONE',  ( 18.62500000000064659, -60.39062499999985079, -7.714727599197336083 ) ) ;
#5820=CARTESIAN_POINT ( 'NONE',  ( -8.043339635997654113, -60.35624999999985363, 8.043339635996302306 ) ) ;
#5827=CIRCLE ( 'NONE', #8087, 3.624999999999999556 ) ;
#5837=CARTESIAN_POINT ( 'NONE',  ( 1.561832610794586740E-12, -94.66249999999980957, -18.62500000000000000 ) ) ;
#5851=CARTESIAN_POINT ( 'NONE',  ( 3.245949991204708063, 2.511656448626708457E-16, -15.01720290182594297 ) ) ;
#5867=CARTESIAN_POINT ( 'NONE',  ( -18.62500000000000000, -84.32499999999977547, -1.562973063126292757E-12 ) ) ;
#5868=CARTESIAN_POINT ( 'NONE',  ( 4.711679271993006068, -46.82812499999987921, 11.37500000000039257 ) ) ;
#5874=CARTESIAN_POINT ( 'NONE',  ( 7.714727599197339636, -13.52812499999996909, 18.62500000000063949 ) ) ;
#5893=CARTESIAN_POINT ( 'NONE',  ( -13.16986379959834252, -80.09374999999982947, -13.16986379960055409 ) ) ;
#5901=CARTESIAN_POINT ( 'NONE',  ( 18.62500000000000000, -42.69999999999988205, 1.560692158462880521E-12 ) ) ;
#5908=CARTESIAN_POINT ( 'NONE',  ( 8.043339635996300530, -14.56874999999996589, 8.043339635997654113 ) ) ;
#5925=CARTESIAN_POINT ( 'NONE',  ( 7.714727599197340524, -104.0281249999997755, 18.62500000000063949 ) ) ;
#5952=CARTESIAN_POINT ( 'NONE',  ( -4.711679271993003404, 2.046875000000014211, -11.37500000000039613 ) ) ;
#5953=CARTESIAN_POINT ( 'NONE',  ( -4.711679271993003404, -71.80312499999982379, -11.37500000000039435 ) ) ;
#5959=CARTESIAN_POINT ( 'NONE',  ( 7.714727599200458030, -86.37187499999978968, -18.62499999999935341 ) ) ;
#5980=CARTESIAN_POINT ( 'NONE',  ( -13.16986379960055409, -84.25624999999983800, 13.16986379959834252 ) ) ;
#5989=CARTESIAN_POINT ( 'NONE',  ( -9.552639591052204498E-13, -5.237499999999969624, 11.37500000000000178 ) ) ;
#5997=CARTESIAN_POINT ( 'NONE',  ( -8.043339635996302306, -72.84374999999981526, -8.043339635997654113 ) ) ;
#6014=CARTESIAN_POINT ( 'NONE',  ( 18.62500000000000000, 0.000000000000000000, 1.560692158462880521E-12 ) ) ;
#6041=CARTESIAN_POINT ( 'NONE',  ( -11.37499999999960743, -33.33437499999990195, -4.711679271994912099 ) ) ;
#6042=CARTESIAN_POINT ( 'NONE',  ( -11.37500000000000000, -41.62499999999990052, -9.545674412382054647E-13 ) ) ;
#6047=CARTESIAN_POINT ( 'NONE',  ( 7.714727599197339636, -30.17812499999993037, 18.62500000000063949 ) ) ;
#6066=CARTESIAN_POINT ( 'NONE',  ( -1.564113515457998370E-12, -102.9874999999997698, 18.62500000000000000 ) ) ;
#6070=B_SPLINE_CURVE_WITH_KNOTS ( 'NONE', 3,
 ( #17003, #10484, #10397, #3487, #5092, #13120, #7570, #14342, #2230, #15754, #2318, #3664, #1009, #9076, #7746, #15845, #3752, #14514, #17266, #5178, #10570, #15931, #2842, #8009, #215, #4188, #13546, #10913, #1265, #5269, #6677, #123, #5620, #9341, #1527, #1348, #12060, #7920, #13462, #16017, #6854, #16373, #17437, #8185, #13294, #17356, #8273, #2577, #12232, #13376, #10654, #5351, #6764, #5529, #16282, #10738, #13633, #11002, #16102, #1436, #9602, #12322 ),
 .UNSPECIFIED., .F., .F.,
 ( 4, 2, 2, 2, 2, 2, 2, 2, 2, 2, 2, 2, 2, 2, 2, 2, 2, 2, 2, 2, 2, 2, 2, 2, 2, 2, 2, 2, 2, 2, 4 ),
 ( 9.394995712984629401E-16, 0.002598098089080421499, 0.003897147133620162789, 0.005196196178159904512, 0.007794294267239384490, 0.009093343311779127081, 0.01039239235631886707, 0.01299049044539835052, 0.01428953948993809224, 0.01493906401220796570, 0.01558858853447783743, 0.01623811305674770916, 0.01656287531788264850, 0.01688763757901758783, 0.01721239984015252716, 0.01753716210128746650, 0.01818668662355734517, 0.01883621114582722383, 0.01948573566809710250, 0.02078478471263685290, 0.02208383375717660677, 0.02338288280171636063, 0.02468193184625611450, 0.02598098089079587183, 0.02857907897987538304, 0.03117717706895489424, 0.03377527515803439850, 0.03507432420257414890, 0.03637337324711390624, 0.03897147133619342091, 0.04156956942527292864 ),
 .UNSPECIFIED. ) ;
#6077=CARTESIAN_POINT ( 'NONE',  ( -11.37500000000039790, -35.41562499999989200, 4.711679271993001628 ) ) ;
#6086=CARTESIAN_POINT ( 'NONE',  ( -11.37500000000000000, -91.57499999999977547, -9.545674412382054647E-13 ) ) ;
#6101=CARTESIAN_POINT ( 'NONE',  ( -1.564113515457998572E-12, -45.78749999999988773, 18.62500000000000000 ) ) ;
#6103=CARTESIAN_POINT ( 'NONE',  ( -18.62500000000064659, -42.66562499999989200, 7.714727599197335195 ) ) ;
#6119=CARTESIAN_POINT ( 'NONE',  ( -8.043339635996300530, -13.49374999999998614, -8.043339635997652337 ) ) ;
#6129=CARTESIAN_POINT ( 'NONE',  ( 13.16986379960055409, -78.08124999999978400, -13.16986379959834430 ) ) ;
#6134=CARTESIAN_POINT ( 'NONE',  ( -7.714727599200466912, -78.04687499999982947, 18.62499999999934985 ) ) ;
#6156=CARTESIAN_POINT ( 'NONE',  ( -13.16986379960055231, -27.05624999999993463, 13.16986379959834252 ) ) ;
#6163=CARTESIAN_POINT ( 'NONE',  ( -4.711679271994916540, -20.84687499999993321, 11.37499999999960565 ) ) ;
#6170=CARTESIAN_POINT ( 'NONE',  ( -8.043339635997652337, -17.65624999999997513, 8.043339635996300530 ) ) ;
#6181=CARTESIAN_POINT ( 'NONE',  ( -18.62500000000000000, -58.27499999999986358, -1.562973063126292555E-12 ) ) ;
#6182=CARTESIAN_POINT ( 'NONE',  ( 18.62362042714189059, -100.0000000000000000, 0.000000000000000000 ) ) ;
#6184=CARTESIAN_POINT ( 'NONE',  ( -13.16986379959834252, -6.243749999999985256, -13.16986379960055054 ) ) ;
#6200=CARTESIAN_POINT ( 'NONE',  ( -4.711679271993001628, -62.40312499999986073, -11.37500000000039613 ) ) ;
#6209=CARTESIAN_POINT ( 'NONE',  ( 8.043339635997652337, -28.13124999999991260, -8.043339635996304082 ) ) ;
#6210=CARTESIAN_POINT ( 'NONE',  ( -11.37500000000039613, -92.61562499999978115, 4.711679271993001628 ) ) ;
#6214=CARTESIAN_POINT ( 'NONE',  ( -7.714727599200466912, -44.74687499999989626, 18.62499999999934985 ) ) ;
#6234=CARTESIAN_POINT ( 'NONE',  ( -13.16986379959834252, -39.54374999999990337, -13.16986379960055054 ) ) ;
#6244=CARTESIAN_POINT ( 'NONE',  ( -11.37500000000039790, -52.06562499999986926, 4.711679271993001628 ) ) ;
#6251=CARTESIAN_POINT ( 'NONE',  ( 8.043339635997652337, -42.63124999999990905, -8.043339635996302306 ) ) ;
#6261=CARTESIAN_POINT ( 'NONE',  ( -7.714727599197335195, -71.80312499999982379, -18.62500000000064304 ) ) ;
#6263=CARTESIAN_POINT ( 'NONE',  ( 13.16986379959834075, -31.21874999999992539, 13.16986379960055231 ) ) ;
#6265=CARTESIAN_POINT ( 'NONE',  ( -7.714727599200467800, -28.09687499999992966, 18.62499999999934630 ) ) ;
#6284=CARTESIAN_POINT ( 'NONE',  ( -8.043339635996300530, -63.44374999999985931, -8.043339635997652337 ) ) ;
#6295=CARTESIAN_POINT ( 'NONE',  ( -4.711679271994916540, -54.14687499999985931, 11.37499999999960565 ) ) ;
#6299=CARTESIAN_POINT ( 'NONE',  ( 13.16986379959834075, -64.51874999999984084, 13.16986379960055231 ) ) ;
#6321=CARTESIAN_POINT ( 'NONE',  ( 18.62500000000064304, -1.040624999999997469, -7.714727599197335195 ) ) ;
#6329=CARTESIAN_POINT ( 'NONE',  ( 4.711679271994911211, -62.47187499999984084, -11.37499999999960743 ) ) ;
#6339=CARTESIAN_POINT ( 'NONE',  ( 8.043339635997652337, -25.98124999999995310, -8.043339635996302306 ) ) ;
#6349=CARTESIAN_POINT ( 'NONE',  ( 18.62499999999934630, -82.20937499999980957, 7.714727599200467800 ) ) ;
#6351=CARTESIAN_POINT ( 'NONE',  ( 13.16986379960055054, -52.03124999999987921, -13.16986379959834430 ) ) ;
#6353=CARTESIAN_POINT ( 'NONE',  ( 13.16986379960055054, -18.73124999999995666, -13.16986379959834430 ) ) ;
#6374=CARTESIAN_POINT ( 'NONE',  ( 11.37500000000039613, -74.89062499999985789, -4.711679271993002516 ) ) ;
#6385=CARTESIAN_POINT ( 'NONE',  ( -9.552639591052204498E-13, -38.53749999999988063, 11.37500000000000178 ) ) ;
#6413=CARTESIAN_POINT ( 'NONE',  ( -18.62499999999934985, -90.53437499999978400, -7.714727599200458918 ) ) ;
#6421=DIRECTION ( 'NONE',  ( 1.000000000000000000, 0.000000000000000000, -0.000000000000000000 ) ) ;
#6422=CARTESIAN_POINT ( 'NONE',  ( 8.043339635997652337, -78.08124999999978400, -8.043339635996304082 ) ) ;
#6432=CARTESIAN_POINT ( 'NONE',  ( 11.37499999999999645, -23.89999999999996305, 9.531744055041752924E-13 ) ) ;
#6439=CARTESIAN_POINT ( 'NONE',  ( -7.714727599197334307, 2.046875000000014211, -18.62500000000064659 ) ) ;
#6441=CARTESIAN_POINT ( 'NONE',  ( -13.16986379959834252, -39.54374999999990337, -13.16986379960055054 ) ) ;
#6443=CARTESIAN_POINT ( 'NONE',  ( 13.16986379960055054, -68.68124999999983515, -13.16986379959834430 ) ) ;
#6463=CARTESIAN_POINT ( 'NONE',  ( 8.043339635997652337, -42.63124999999990905, -8.043339635996302306 ) ) ;
#6472=CARTESIAN_POINT ( 'NONE',  ( -9.552639591052204498E-13, -71.83749999999979252, 11.37500000000000178 ) ) ;
#6473=CARTESIAN_POINT ( 'NONE',  ( 8.043339635996300530, -97.81874999999976694, 8.043339635997654113 ) ) ;
#6501=CARTESIAN_POINT ( 'NONE',  ( -7.714727599197335195, -71.80312499999982379, -18.62500000000064304 ) ) ;
#6512=CARTESIAN_POINT ( 'NONE',  ( -11.37500000000000000, -24.97499999999994102, -9.545674412382054647E-13 ) ) ;
#6521=CARTESIAN_POINT ( 'NONE',  ( 7.714727599200456254, -10.37187499999999396, -18.62499999999935341 ) ) ;
#6528=PRODUCT_DEFINITION_FORMATION_WITH_SPECIFIED_SOURCE ( 'ANY', '', #2950, .NOT_KNOWN. ) ;
#6529=CARTESIAN_POINT ( 'NONE',  ( -13.16986379960055231, -93.65624999999977263, 13.16986379959834252 ) ) ;
#6531=CARTESIAN_POINT ( 'NONE',  ( -7.714727599197334307, -14.60312499999994706, -18.62500000000064659 ) ) ;
#6533=CARTESIAN_POINT ( 'NONE',  ( -7.714727599197335195, -88.45312499999978684, -18.62500000000064304 ) ) ;
#6549=CARTESIAN_POINT ( 'NONE',  ( -8.043339635996300530, -46.79374999999990337, -8.043339635997652337 ) ) ;
#6559=CARTESIAN_POINT ( 'NONE',  ( 8.043339635997652337, -78.08124999999978400, -8.043339635996304082 ) ) ;
#6564=CARTESIAN_POINT ( 'NONE',  ( 7.714727599197339636, -96.77812499999977547, 18.62500000000063949 ) ) ;
#6586=CARTESIAN_POINT ( 'NONE',  ( -7.714727599200467800, -78.04687499999982947, 18.62499999999934630 ) ) ;
#6596=CARTESIAN_POINT ( 'NONE',  ( 4.711679271994909435, -36.42187499999990763, -11.37499999999960387 ) ) ;
#6607=CARTESIAN_POINT ( 'NONE',  ( -8.043339635996300530, -80.09374999999982947, -8.043339635997652337 ) ) ;
#6612=CARTESIAN_POINT ( 'NONE',  ( 13.16986379960055409, -61.43124999999983515, -13.16986379959834430 ) ) ;
#6614=CARTESIAN_POINT ( 'NONE',  ( 18.62500000000064304, -84.29062499999983515, -7.714727599197335195 ) ) ;
#6636=CARTESIAN_POINT ( 'NONE',  ( -4.711679271993001628, -95.70312499999977263, -11.37500000000039613 ) ) ;
#6643=CARTESIAN_POINT ( 'NONE',  ( 11.37500000000000178, -75.99999999999980105, 9.531744055041752924E-13 ) ) ;
#6644=CARTESIAN_POINT ( 'NONE',  ( -1.564113515457998572E-12, -12.48749999999997051, 18.62500000000000000 ) ) ;
#6666=CARTESIAN_POINT ( 'NONE',  ( -18.62500000000064659, -59.31562499999985505, 7.714727599197335195 ) ) ;
#6677=CARTESIAN_POINT ( 'NONE',  ( 3.892042677208999546, -100.0000000000000284, 14.96341192791908092 ) ) ;
#6679=CARTESIAN_POINT ( 'NONE',  ( -4.711679271993004292, -21.85312499999995239, -11.37500000000039435 ) ) ;
#6688=CARTESIAN_POINT ( 'NONE',  ( 18.62500000000000000, -7.250000000000001776, 1.560692158462880521E-12 ) ) ;
#6695=CARTESIAN_POINT ( 'NONE',  ( 18.62500000000000000, -42.69999999999988205, 1.560692158462880521E-12 ) ) ;
#6697=CARTESIAN_POINT ( 'NONE',  ( 13.16986379959834075, -81.16874999999980389, 13.16986379960055231 ) ) ;
#6699=CARTESIAN_POINT ( 'NONE',  ( -13.16986379960055231, -77.00624999999982379, 13.16986379959834252 ) ) ;
#6719=CARTESIAN_POINT ( 'NONE',  ( -18.62500000000000000, -15.57499999999998153, -1.562973063126292757E-12 ) ) ;
#6728=CARTESIAN_POINT ( 'NONE',  ( -11.37500000000000000, -24.97499999999994102, -9.545674412382054647E-13 ) ) ;
#6729=CARTESIAN_POINT ( 'NONE',  ( 1.561832610794586538E-12, -4.162499999999989875, -18.62500000000000000 ) ) ;
#6748=CARTESIAN_POINT ( 'NONE',  ( -11.37500000000000000, -8.324999999999979750, -9.545674412382054647E-13 ) ) ;
#6752=CARTESIAN_POINT ( 'NONE',  ( 7.714727599197338748, -63.47812499999984226, 18.62500000000063949 ) ) ;
#6764=CARTESIAN_POINT ( 'NONE',  ( 16.45599557390471546, -100.0000000000000142, 8.218326127789341129 ) ) ;
#6766=CARTESIAN_POINT ( 'NONE',  ( -11.37499999999960387, -40.58437499999990905, -4.711679271994910323 ) ) ;
#6774=CARTESIAN_POINT ( 'NONE',  ( -11.37499999999960210, -81.13437499999982094, -4.711679271994911211 ) ) ;
#6783=CARTESIAN_POINT ( 'NONE',  ( 7.714727599197340524, -39.57812499999989342, 18.62500000000063949 ) ) ;
#6785=CARTESIAN_POINT ( 'NONE',  ( 1.561832610794586740E-12, -30.21249999999990976, -18.62500000000000000 ) ) ;
#6807=CARTESIAN_POINT ( 'NONE',  ( 7.714727599197340524, -37.42812499999993037, 18.62500000000063949 ) ) ;
#6817=CARTESIAN_POINT ( 'NONE',  ( -11.37500000000000000, -41.62499999999990052, -9.545674412382054647E-13 ) ) ;
#6818=CARTESIAN_POINT ( 'NONE',  ( 18.62499999999934630, -32.25937499999992042, 7.714727599200467800 ) ) ;
#6823=CARTESIAN_POINT ( 'NONE',  ( 16.37694731117742464, 1.089405092048505075E-13, -8.432838350389969762 ) ) ;
#6854=CARTESIAN_POINT ( 'NONE',  ( 8.006520823759419869, -99.99999999999997158, 15.10378497192285785 ) ) ;
#6856=CARTESIAN_POINT ( 'NONE',  ( -8.043339635996302306, -89.49374999999979252, -8.043339635997654113 ) ) ;
#6857=DIRECTION ( 'NONE',  ( -1.000000000000000000, 0.000000000000000000, 0.000000000000000000 ) ) ;
#6868=CARTESIAN_POINT ( 'NONE',  ( -4.711679271994915652, -85.29687499999980105, 11.37499999999960210 ) ) ;
#6875=CARTESIAN_POINT ( 'NONE',  ( 7.714727599197340524, -22.92812499999992326, 18.62500000000063949 ) ) ;
#6878=CARTESIAN_POINT ( 'NONE',  ( 18.62499999999934630, -98.85937499999975842, 7.714727599200467800 ) ) ;
#6901=CARTESIAN_POINT ( 'NONE',  ( 18.62500000000064659, -41.59062499999991758, -7.714727599197336083 ) ) ;
#6913=CARTESIAN_POINT ( 'NONE',  ( 3.077395063295970790, 9.636628673746354086E-15, -14.72315406558967688 ) ) ;
#6927=CARTESIAN_POINT ( 'NONE',  ( -9.552639591052204498E-13, -12.48749999999997051, 11.37500000000000000 ) ) ;
#6945=CARTESIAN_POINT ( 'NONE',  ( -11.37499999999960387, -57.23437499999987921, -4.711679271994910323 ) ) ;
#6956=CARTESIAN_POINT ( 'NONE',  ( -13.16986379959834252, -46.79374999999990337, -13.16986379960055409 ) ) ;
#6963=CARTESIAN_POINT ( 'NONE',  ( 7.714727599200456254, -62.47187499999984084, -18.62499999999935341 ) ) ;
#6965=CARTESIAN_POINT ( 'NONE',  ( -18.62500000000064659, -52.06562499999986926, 7.714727599197333419 ) ) ;
#6989=CARTESIAN_POINT ( 'NONE',  ( 8.043339635997652337, -92.58124999999978400, -8.043339635996302306 ) ) ;
#6995=CARTESIAN_POINT ( 'NONE',  ( 15.00000000000000000, 0.000000000000000000, 1.256933281983527907E-12 ) ) ;
#7002=CARTESIAN_POINT ( 'NONE',  ( 8.627630420782578469, 5.967892910702088472E-16, -8.354871048539219913 ) ) ;
#7019=ORIENTED_EDGE ( 'NONE', *, *, #2974, .T. ) ;
#7025=CARTESIAN_POINT ( 'NONE',  ( 18.62500000000000000, 0.000000000000000000, 1.560692158462880521E-12 ) ) ;
#7031=FACE_OUTER_BOUND ( 'NONE', #11935, .T. ) ;
#7036=CARTESIAN_POINT ( 'NONE',  ( -8.043339635997654113, -60.35624999999985363, 8.043339635996302306 ) ) ;
#7046=CARTESIAN_POINT ( 'NONE',  ( 7.714727599200456254, -43.67187499999991473, -18.62499999999935341 ) ) ;
#7052=CARTESIAN_POINT ( 'NONE',  ( -18.62499999999935341, -83.28437499999976978, -7.714727599200458030 ) ) ;
#7073=CARTESIAN_POINT ( 'NONE',  ( 13.16986379959833897, -71.76874999999985505, 13.16986379960055409 ) ) ;
#7079=DIRECTION ( 'NONE',  ( -1.000000000000000000, 0.000000000000000000, -8.379555213223520053E-14 ) ) ;
#7085=CARTESIAN_POINT ( 'NONE',  ( 4.295984800146390725, -1.623771540349147248E-16, -12.82069415802188672 ) ) ;
#7087=AXIS2_PLACEMENT_3D ( 'NONE', #3462, #11515, #12749 ) ;
#7101=CARTESIAN_POINT ( 'NONE',  ( 11.37499999999960210, -65.55937499999983231, 4.711679271994917428 ) ) ;
#7118=CARTESIAN_POINT ( 'NONE',  ( 9.538709233711902776E-13, -87.41249999999979536, -11.37500000000000000 ) ) ;
#7126=VERTEX_POINT ( 'NONE', #10244 ) ;
#7127=CARTESIAN_POINT ( 'NONE',  ( -1.564113515457998370E-12, -19.73749999999997229, 18.62500000000000000 ) ) ;
#7135=CARTESIAN_POINT ( 'NONE',  ( 11.37500000000000178, 7.250000000000001776, 9.531744055041752924E-13 ) ) ;
#7142=CARTESIAN_POINT ( 'NONE',  ( 11.37499999999960210, -65.55937499999984652, 4.711679271994918317 ) ) ;
#7159=CARTESIAN_POINT ( 'NONE',  ( 7.714727599197340524, -54.07812499999989342, 18.62500000000063949 ) ) ;
#7170=CARTESIAN_POINT ( 'NONE',  ( 5.292333123709091147, 1.381986750645590742E-15, -11.92816106025346556 ) ) ;
#7183=CARTESIAN_POINT ( 'NONE',  ( -1.564113515457998370E-12, -88.48749999999975557, 18.62500000000000000 ) ) ;
#7184=CARTESIAN_POINT ( 'NONE',  ( -4.711679271994915652, -28.09687499999992966, 11.37499999999960210 ) ) ;
#7189=CARTESIAN_POINT ( 'NONE',  ( -18.62500000000064659, -9.365624999999976552, 7.714727599197333419 ) ) ;
#7210=CARTESIAN_POINT ( 'NONE',  ( 1.561832610794586740E-12, -78.01249999999983231, -18.62500000000000000 ) ) ;
#7218=CARTESIAN_POINT ( 'NONE',  ( 4.711679271994911211, 4.128125000000008704, -11.37499999999960743 ) ) ;
#7225=CARTESIAN_POINT ( 'NONE',  ( 8.043339635996300530, -47.86874999999988489, 8.043339635997654113 ) ) ;
#7242=CARTESIAN_POINT ( 'NONE',  ( -13.16986379960055409, -84.25624999999983800, 13.16986379959834252 ) ) ;
#7270=CARTESIAN_POINT ( 'NONE',  ( 11.37499999999960565, -8.359374999999960920, 4.711679271994918317 ) ) ;
#7271=CARTESIAN_POINT ( 'NONE',  ( -11.37499999999960387, -57.23437499999987921, -4.711679271994911211 ) ) ;
#7272=VERTEX_POINT ( 'NONE', #12966 ) ;
#7277=CARTESIAN_POINT ( 'NONE',  ( 13.16986379960055054, -18.73124999999995666, -13.16986379959834430 ) ) ;
#7298=CARTESIAN_POINT ( 'NONE',  ( -18.62499999999935341, -47.83437499999990195, -7.714727599200458030 ) ) ;
#7306=CARTESIAN_POINT ( 'NONE',  ( -8.043339635996304082, -65.59374999999981526, -8.043339635997652337 ) ) ;
#7314=CARTESIAN_POINT ( 'NONE',  ( -4.711679271993004292, -21.85312499999995239, -11.37500000000039435 ) ) ;
#7333=CARTESIAN_POINT ( 'NONE',  ( 18.62500000000000000, -73.84999999999983800, 1.560692158462880521E-12 ) ) ;
#7363=CARTESIAN_POINT ( 'NONE',  ( -8.043339635996304082, -32.29374999999990337, -8.043339635997652337 ) ) ;
#7364=CARTESIAN_POINT ( 'NONE',  ( -9.552639591052204498E-13, -29.13749999999993179, 11.37500000000000000 ) ) ;
#7367=CARTESIAN_POINT ( 'NONE',  ( -13.16986379959834252, -56.19374999999985931, -13.16986379960055054 ) ) ;
#7391=CARTESIAN_POINT ( 'NONE',  ( 1.561832610794586740E-12, -94.66249999999980957, -18.62500000000000000 ) ) ;
#7398=CARTESIAN_POINT ( 'NONE',  ( -8.043339635996304082, -15.64374999999994387, -8.043339635997652337 ) ) ;
#7406=CARTESIAN_POINT ( 'NONE',  ( -8.043339635997652337, -34.30624999999993463, 8.043339635996300530 ) ) ;
#7423=CARTESIAN_POINT ( 'NONE',  ( 13.16986379960055054, -18.73124999999995666, -13.16986379959834430 ) ) ;
#7425=CARTESIAN_POINT ( 'NONE',  ( -7.714727599200466912, -51.99687499999990337, 18.62499999999935341 ) ) ;
#7443=CARTESIAN_POINT ( 'NONE',  ( -11.37500000000039613, -59.31562499999985505, 4.711679271993002516 ) ) ;
#7452=CARTESIAN_POINT ( 'NONE',  ( 11.37500000000039613, -10.44062499999995453, -4.711679271993004292 ) ) ;
#7453=CARTESIAN_POINT ( 'NONE',  ( 11.37500000000000000, -33.29999999999991900, 9.531744055041752924E-13 ) ) ;
#7457=CARTESIAN_POINT ( 'NONE',  ( -1.564113515457998572E-12, -45.78749999999988773, 18.62500000000000000 ) ) ;
#7461=ADVANCED_FACE ( 'NONE', ( #7031 ), #2750, .T. ) ;
#7477=CARTESIAN_POINT ( 'NONE',  ( -18.62499999999934985, -23.93437499999993889, -7.714727599200458918 ) ) ;
#7485=CARTESIAN_POINT ( 'NONE',  ( 4.711679271994911211, -45.82187499999987779, -11.37499999999960743 ) ) ;
#7492=CARTESIAN_POINT ( 'NONE',  ( 11.37499999999960210, -22.85937499999996092, 4.711679271994916540 ) ) ;
#7505=CARTESIAN_POINT ( 'NONE',  ( 7.714727599200458030, -53.07187499999987068, -18.62499999999934985 ) ) ;
#7507=CARTESIAN_POINT ( 'NONE',  ( 13.16986379960055054, -52.03124999999987921, -13.16986379959834430 ) ) ;
#7519=CARTESIAN_POINT ( 'NONE',  ( 10.91662889535533232, 1.083605698617470082E-14, -3.544256338779125937 ) ) ;
#7526=CARTESIAN_POINT ( 'NONE',  ( -8.043339635997652337, -67.60624999999984652, 8.043339635996300530 ) ) ;
#7535=CARTESIAN_POINT ( 'NONE',  ( -4.711679271994916540, -20.84687499999993321, 11.37499999999960565 ) ) ;
#7542=CARTESIAN_POINT ( 'NONE',  ( -13.16986379960055231, -43.70624999999989768, 13.16986379959834252 ) ) ;
#7561=CARTESIAN_POINT ( 'NONE',  ( 1.561832610794586538E-12, -37.46249999999991331, -18.62500000000000000 ) ) ;
#7570=CARTESIAN_POINT ( 'NONE',  ( 10.59289456970070553, -99.99999999999994316, 4.700358225852117933 ) ) ;
#7572=CARTESIAN_POINT ( 'NONE',  ( -11.37499999999960743, -16.68437499999993889, -4.711679271994912099 ) ) ;
#7579=CARTESIAN_POINT ( 'NONE',  ( -8.043339635997654113, -93.65624999999977263, 8.043339635996302306 ) ) ;
#7588=CARTESIAN_POINT ( 'NONE',  ( 13.16986379959834075, -47.86874999999988489, 13.16986379960055231 ) ) ;
#7591=CARTESIAN_POINT ( 'NONE',  ( 13.16986379959834075, -64.51874999999984084, 13.16986379960055231 ) ) ;
#7593=AXIS2_PLACEMENT_3D ( 'NONE', #16461, #1525, #8272 ) ;
#7594=CARTESIAN_POINT ( 'NONE',  ( 13.16986379959834075, -14.56874999999996589, 13.16986379960055231 ) ) ;
#7614=CARTESIAN_POINT ( 'NONE',  ( 11.37500000000039613, -58.24062499999988063, -4.711679271993002516 ) ) ;
#7624=CARTESIAN_POINT ( 'NONE',  ( -9.552639591052204498E-13, -88.48749999999975557, 11.37500000000000178 ) ) ;
#7627=CARTESIAN_POINT ( 'NONE',  ( 13.16986379960055054, -68.68124999999983515, -13.16986379959834430 ) ) ;
#7652=CARTESIAN_POINT ( 'NONE',  ( -1.564113515457998572E-12, -29.13749999999993179, 18.62500000000000000 ) ) ;
#7660=( GEOMETRIC_REPRESENTATION_CONTEXT ( 3 ) GLOBAL_UNCERTAINTY_ASSIGNED_CONTEXT ( ( #11405 ) ) GLOBAL_UNIT_ASSIGNED_CONTEXT ( ( #529, #14124, #16870 ) ) REPRESENTATION_CONTEXT ( 'NONE', 'WORKASPACE' ) );
#7661=CARTESIAN_POINT ( 'NONE',  ( 18.62500000000000000, 0.000000000000000000, 1.560692158462880521E-12 ) ) ;
#7662=CARTESIAN_POINT ( 'NONE',  ( 11.37500000000000178, -59.34999999999983800, 9.531744055041752924E-13 ) ) ;
#7668=CARTESIAN_POINT ( 'NONE',  ( -11.37500000000039613, -16.61562499999998010, 4.711679271993000739 ) ) ;
#7677=CARTESIAN_POINT ( 'NONE',  ( 1.561832610794586740E-12, 3.087500000000011458, -18.62500000000000000 ) ) ;
#7679=CARTESIAN_POINT ( 'NONE',  ( 13.16986379960055054, -35.38124999999991616, -13.16986379959834430 ) ) ;
#7681=CARTESIAN_POINT ( 'NONE',  ( 18.62499999999934630, -65.55937499999984652, 7.714727599200467800 ) ) ;
#7699=CARTESIAN_POINT ( 'NONE',  ( 11.37500000000039613, -41.59062499999991758, -4.711679271993002516 ) ) ;
#7709=CARTESIAN_POINT ( 'NONE',  ( 4.711679271994909435, -3.121874999999992184, -11.37499999999960387 ) ) ;
#7710=CARTESIAN_POINT ( 'NONE',  ( -11.37499999999960387, -90.53437499999978400, -4.711679271994911211 ) ) ;
#7713=CARTESIAN_POINT ( 'NONE',  ( 13.16986379960055054, -85.33124999999978400, -13.16986379959834430 ) ) ;
#7737=CARTESIAN_POINT ( 'NONE',  ( -13.16986379960055231, -93.65624999999977263, 13.16986379959834252 ) ) ;
#7746=CARTESIAN_POINT ( 'NONE',  ( 6.601226367162849940, -99.99999999999998579, 10.86885066916123321 ) ) ;
#7748=CARTESIAN_POINT ( 'NONE',  ( 8.043339635997654113, -18.73124999999995666, -8.043339635996304082 ) ) ;
#7759=CARTESIAN_POINT ( 'NONE',  ( 11.37499999999960210, -98.85937499999975842, 4.711679271994918317 ) ) ;
#7770=CARTESIAN_POINT ( 'NONE',  ( 18.62500000000000000, -99.89999999999976410, 1.560692158462880521E-12 ) ) ;
#7772=CARTESIAN_POINT ( 'NONE',  ( -18.62500000000064659, -75.96562499999980389, 7.714727599197335195 ) ) ;
#7774=CARTESIAN_POINT ( 'NONE',  ( -7.714727599200467800, -61.39687499999984510, 18.62499999999934630 ) ) ;
#7793=CARTESIAN_POINT ( 'NONE',  ( 4.711679271993006957, -37.42812499999992326, 11.37500000000039257 ) ) ;
#7803=CARTESIAN_POINT ( 'NONE',  ( -4.711679271993003404, -81.20312499999978684, -11.37500000000039613 ) ) ;
#7829=CARTESIAN_POINT ( 'NONE',  ( 13.16986379960055054, -85.33124999999978400, -13.16986379959834430 ) ) ;
#7837=CARTESIAN_POINT ( 'NONE',  ( -8.043339635996304082, -82.24374999999977831, -8.043339635997652337 ) ) ;
#7845=CARTESIAN_POINT ( 'NONE',  ( 18.62500000000064659, -8.290625000000000355, -7.714727599197336083 ) ) ;
#7851=CARTESIAN_POINT ( 'NONE',  ( 18.62500000000000000, -83.24999999999980105, 1.560692158462880521E-12 ) ) ;
#7853=CARTESIAN_POINT ( 'NONE',  ( -13.16986379959834252, 1.006250000000015854, -13.16986379960055409 ) ) ;
#7874=CARTESIAN_POINT ( 'NONE',  ( -4.711679271993001628, -29.10312499999994884, -11.37500000000039613 ) ) ;
#7884=CARTESIAN_POINT ( 'NONE',  ( -4.711679271993004292, -5.203124999999986677, -11.37500000000039435 ) ) ;
#7912=CARTESIAN_POINT ( 'NONE',  ( -18.62500000000000000, -74.92499999999982663, -1.562973063126292555E-12 ) ) ;
#7920=CARTESIAN_POINT ( 'NONE',  ( 6.303891475472711114, -100.0000000000000568, 15.41241088168433926 ) ) ;
#7922=CARTESIAN_POINT ( 'NONE',  ( 11.37500000000039435, -17.69062499999995453, -4.711679271993004292 ) ) ;
#7930=CARTESIAN_POINT ( 'NONE',  ( -9.552639591052204498E-13, -86.33749999999982094, 11.37499999999999645 ) ) ;
#7938=CARTESIAN_POINT ( 'NONE',  ( 18.62500000000064304, -50.99062499999987352, -7.714727599197335195 ) ) ;
#7940=CARTESIAN_POINT ( 'NONE',  ( 18.62499999999935341, -25.00937499999992397, 7.714727599200469577 ) ) ;
#7942=CARTESIAN_POINT ( 'NONE',  ( 18.62499999999934630, -82.20937499999980957, 7.714727599200467800 ) ) ;
#7962=CARTESIAN_POINT ( 'NONE',  ( 11.37499999999960210, -106.1093749999997584, 4.711679271994916540 ) ) ;
#7971=CARTESIAN_POINT ( 'NONE',  ( -4.711679271994916540, -70.79687499999981526, 11.37499999999960565 ) ) ;
#7972=CARTESIAN_POINT ( 'NONE',  ( 13.16986379959834075, -31.21874999999992539, 13.16986379960055231 ) ) ;
#7994=CARTESIAN_POINT ( 'NONE',  ( 8.043339635996300530, -14.56874999999996589, 8.043339635997654113 ) ) ;
#7998=CARTESIAN_POINT ( 'NONE',  ( 18.62500000000000000, -66.59999999999983800, 1.560692158462880521E-12 ) ) ;
#8009=CARTESIAN_POINT ( 'NONE',  ( 3.702617594344294272, -100.0000000000000426, 13.96937958327705864 ) ) ;
#8011=CARTESIAN_POINT ( 'NONE',  ( 11.37499999999960210, -15.60937499999996270, 4.711679271994918317 ) ) ;
#8019=CARTESIAN_POINT ( 'NONE',  ( 9.538709233711902776E-13, -61.36249999999986215, -11.37499999999999645 ) ) ;
#8024=CARTESIAN_POINT ( 'NONE',  ( -18.62500000000064659, -35.41562499999989200, 7.714727599197333419 ) ) ;
#8026=CARTESIAN_POINT ( 'NONE',  ( -13.16986379959834252, -32.29374999999990337, -13.16986379960055409 ) ) ;
#8048=CARTESIAN_POINT ( 'NONE',  ( 9.538709233711902776E-13, -94.66249999999979536, -11.37499999999999645 ) ) ;
#8060=CARTESIAN_POINT ( 'NONE',  ( -9.552639591052204498E-13, -12.48749999999997051, 11.37500000000000000 ) ) ;
#8061=CARTESIAN_POINT ( 'NONE',  ( -7.714727599200467800, -44.74687499999989626, 18.62499999999934630 ) ) ;
#8085=CARTESIAN_POINT ( 'NONE',  ( -18.62499999999934985, -57.23437499999987921, -7.714727599200458918 ) ) ;
#8087=AXIS2_PLACEMENT_3D ( 'NONE', #12633, #10964, #5583 ) ;
#8098=CARTESIAN_POINT ( 'NONE',  ( 8.043339635996300530, -14.56874999999996589, 8.043339635997654113 ) ) ;
#8108=CARTESIAN_POINT ( 'NONE',  ( 4.711679271994911211, -60.32187499999988489, -11.37499999999960210 ) ) ;
#8114=CARTESIAN_POINT ( 'NONE',  ( -18.62500000000000000, -34.37499999999990052, -1.562973063126292757E-12 ) ) ;
#8116=CARTESIAN_POINT ( 'NONE',  ( 18.62500000000000000, -9.399999999999959499, 1.560692158462880521E-12 ) ) ;
#8137=CARTESIAN_POINT ( 'NONE',  ( 4.711679271994911211, -93.62187499999978968, -11.37499999999960210 ) ) ;
#8146=CARTESIAN_POINT ( 'NONE',  ( -9.552639591052204498E-13, -62.43749999999985079, 11.37500000000000000 ) ) ;
#8147=CARTESIAN_POINT ( 'NONE',  ( -18.62499999999934985, -7.284374999999982947, -7.714727599200458918 ) ) ;
#8151=CARTESIAN_POINT ( 'NONE',  ( -18.62500000000064659, -92.61562499999978115, 7.714727599197333419 ) ) ;
#8185=CARTESIAN_POINT ( 'NONE',  ( 10.01122869418810524, -99.99999999999997158, 14.34650401988984747 ) ) ;
#8187=CARTESIAN_POINT ( 'NONE',  ( -4.711679271994916540, -61.39687499999984510, 11.37499999999960210 ) ) ;
#8192=ORIENTED_EDGE ( 'NONE', *, *, #2992, .F. ) ;
#8196=CARTESIAN_POINT ( 'NONE',  ( -8.043339635997652337, -67.60624999999984652, 8.043339635996300530 ) ) ;
#8202=PRODUCT_DEFINITION_SHAPE ( 'NONE', 'NONE',  #3939 ) ;
#8203=CARTESIAN_POINT ( 'NONE',  ( 18.62500000000064659, -60.39062499999985079, -7.714727599197336083 ) ) ;
#8205=CARTESIAN_POINT ( 'NONE',  ( -1.564113515457998572E-12, -79.08749999999980673, 18.62500000000000000 ) ) ;
#8223=ADVANCED_FACE ( 'NONE', ( #4410 ), #3069, .F. ) ;
#8229=CARTESIAN_POINT ( 'NONE',  ( -8.043339635996300530, -96.74374999999980673, -8.043339635997652337 ) ) ;
#8238=CARTESIAN_POINT ( 'NONE',  ( -7.714727599197335195, -21.85312499999995239, -18.62500000000064304 ) ) ;
#8265=CARTESIAN_POINT ( 'NONE',  ( -13.16986379959834252, -22.89374999999994387, -13.16986379960055054 ) ) ;
#8272=DIRECTION ( 'NONE',  ( 1.000000000000000000, 0.000000000000000000, 8.379555213223520053E-14 ) ) ;
#8273=CARTESIAN_POINT ( 'NONE',  ( 11.51355534411690762, -100.0000000000000284, 13.49408347815985465 ) ) ;
#8275=CARTESIAN_POINT ( 'NONE',  ( 11.37499999999999645, -7.250000000000000000, 9.531744055041752924E-13 ) ) ;
#8287=CARTESIAN_POINT ( 'NONE',  ( -18.62500000000064659, -49.91562499999989910, 7.714727599197333419 ) ) ;
#8293=CARTESIAN_POINT ( 'NONE',  ( -18.62500000000000000, -17.72499999999994102, -1.562973063126292757E-12 ) ) ;
#8295=CARTESIAN_POINT ( 'NONE',  ( 7.714727599197340524, -39.57812499999989342, 18.62500000000063949 ) ) ;
#8318=CARTESIAN_POINT ( 'NONE',  ( -4.711679271994915652, -101.9468749999997783, 11.37499999999960210 ) ) ;
#8330=CARTESIAN_POINT ( 'NONE',  ( 18.62500000000007105, 1.797534614761401329E-30, -0.8911350689967181271 ) ) ;
#8345=CARTESIAN_POINT ( 'NONE',  ( 4.711679271994910323, -19.77187499999995168, -11.37499999999960387 ) ) ;
#8363=CARTESIAN_POINT ( 'NONE',  ( -4.711679271993004292, -55.15312499999986784, -11.37500000000039435 ) ) ;
#8374=CARTESIAN_POINT ( 'NONE',  ( -18.62500000000064659, -66.56562499999988347, 7.714727599197333419 ) ) ;
#8380=CARTESIAN_POINT ( 'NONE',  ( -18.62500000000000000, -51.02499999999986358, -1.562973063126292757E-12 ) ) ;
#8382=CARTESIAN_POINT ( 'NONE',  ( -1.564113515457998370E-12, -88.48749999999975557, 18.62500000000000000 ) ) ;
#8406=CARTESIAN_POINT ( 'NONE',  ( 1.561832610794586740E-12, -61.36249999999986215, -18.62500000000000000 ) ) ;
#8418=CARTESIAN_POINT ( 'NONE',  ( 10.05114101558813289, -5.362028352459332625E-15, -14.43934216884202293 ) ) ;
#8433=CARTESIAN_POINT ( 'NONE',  ( -4.711679271994915652, -61.39687499999985221, 11.37499999999960210 ) ) ;
#8453=CARTESIAN_POINT ( 'NONE',  ( 8.043339635996300530, -97.81874999999976694, 8.043339635997654113 ) ) ;
#8463=CARTESIAN_POINT ( 'NONE',  ( -1.564113515457998370E-12, -69.68749999999984368, 18.62500000000000000 ) ) ;
#8471=CARTESIAN_POINT ( 'NONE',  ( 18.62499999999935341, -74.95937499999980957, 7.714727599200469577 ) ) ;
#8477=CARTESIAN_POINT ( 'NONE',  ( -9.552639591052204498E-13, -45.78749999999988773, 11.37500000000000000 ) ) ;
#8494=CARTESIAN_POINT ( 'NONE',  ( -13.16986379960055409, -67.60624999999984652, 13.16986379959834252 ) ) ;
#8507=CARTESIAN_POINT ( 'NONE',  ( 18.28134285175915252, 8.384379708534145006E-15, -3.505973352197490733 ) ) ;
#8523=CARTESIAN_POINT ( 'NONE',  ( 11.37500000000039435, -34.34062499999991758, -4.711679271993003404 ) ) ;
#8550=CARTESIAN_POINT ( 'NONE',  ( 18.62500000000000000, -23.89999999999996305, 1.560692158462880521E-12 ) ) ;
#8556=CARTESIAN_POINT ( 'NONE',  ( 18.62499999999935341, -91.60937499999975842, 7.714727599200469577 ) ) ;
#8564=CARTESIAN_POINT ( 'NONE',  ( 11.37500000000000000, -66.59999999999983800, 9.531744055041752924E-13 ) ) ;
#8581=CARTESIAN_POINT ( 'NONE',  ( -7.714727599200466912, -101.9468749999998067, 18.62499999999935341 ) ) ;
#8587=LINE ( 'NONE', #6995, #446 ) ;
#8607=CARTESIAN_POINT ( 'NONE',  ( 4.711679271994911211, -12.52187499999995524, -11.37499999999960743 ) ) ;
#8608=CARTESIAN_POINT ( 'NONE',  ( -9.552639591052204498E-13, -79.08749999999980673, 11.37500000000000000 ) ) ;
#8614=CARTESIAN_POINT ( 'NONE',  ( 1.561832610794586538E-12, -4.162499999999989875, -18.62500000000000000 ) ) ;
#8623=( LENGTH_UNIT ( ) NAMED_UNIT ( * ) SI_UNIT ( .MILLI., .METRE. ) );
#8636=CARTESIAN_POINT ( 'NONE',  ( -18.62499999999935341, -81.13437499999982094, -7.714727599200458030 ) ) ;
#8643=CARTESIAN_POINT ( 'NONE',  ( -11.37500000000000178, -1.074999999999978639, -9.545674412382054647E-13 ) ) ;
#8650=CARTESIAN_POINT ( 'NONE',  ( 4.711679271993006068, -30.17812499999993747, 11.37500000000039257 ) ) ;
#8666=CARTESIAN_POINT ( 'NONE',  ( -18.62499999999934985, -7.284374999999982947, -7.714727599200458918 ) ) ;
#8668=CARTESIAN_POINT ( 'NONE',  ( 7.714727599200456254, -60.32187499999988489, -18.62499999999935341 ) ) ;
#8693=CARTESIAN_POINT ( 'NONE',  ( 8.043339635997652337, -11.48124999999995488, -8.043339635996304082 ) ) ;
#8694=CARTESIAN_POINT ( 'NONE',  ( 4.711679271993006068, -30.17812499999993037, 11.37500000000039257 ) ) ;
#8699=CARTESIAN_POINT ( 'NONE',  ( 7.714727599197339636, -46.82812499999987921, 18.62500000000063949 ) ) ;
#8719=CARTESIAN_POINT ( 'NONE',  ( 18.62500000000064304, -17.69062499999995453, -7.714727599197335195 ) ) ;
#8729=CARTESIAN_POINT ( 'NONE',  ( 11.37500000000039613, -10.44062499999995453, -4.711679271993004292 ) ) ;
#8737=CARTESIAN_POINT ( 'NONE',  ( -11.37499999999960387, -90.53437499999978400, -4.711679271994910323 ) ) ;
#8755=CARTESIAN_POINT ( 'NONE',  ( -18.62500000000000000, -41.62499999999990052, -1.562973063126292555E-12 ) ) ;
#8757=CARTESIAN_POINT ( 'NONE',  ( 18.62500000000064659, -74.89062499999985789, -7.714727599197336083 ) ) ;
#8773=DIRECTION ( 'NONE',  ( 0.000000000000000000, 0.000000000000000000, 1.000000000000000000 ) ) ;
#8774=CARTESIAN_POINT ( 'NONE',  ( 4.711679271994909435, -69.72187499999982663, -11.37499999999960387 ) ) ;
#8783=CARTESIAN_POINT ( 'NONE',  ( -13.16986379959834252, -82.24374999999977831, -13.16986379960055409 ) ) ;
#8784=CARTESIAN_POINT ( 'NONE',  ( -4.711679271993003404, -38.50312499999991189, -11.37500000000039435 ) ) ;
#8787=CARTESIAN_POINT ( 'NONE',  ( -18.62500000000000000, -74.92499999999982663, -1.562973063126292555E-12 ) ) ;
#8808=CARTESIAN_POINT ( 'NONE',  ( 1.561832610794586538E-12, -20.81249999999995026, -18.62500000000000000 ) ) ;
#8818=CARTESIAN_POINT ( 'NONE',  ( -11.37500000000039790, -18.76562499999993605, 4.711679271993001628 ) ) ;
#8825=CARTESIAN_POINT ( 'NONE',  ( -9.552639591052204498E-13, -95.73749999999976978, 11.37500000000000000 ) ) ;
#8830=B_SPLINE_CURVE_WITH_KNOTS ( 'NONE', 3,
 ( #4513, #8330, #3167, #8507, #9568, #5591, #2987, #11144, #12201, #6823, #93, #15088, #13856, #5498, #1498, #10880, #11233, #16608, #9921, #8418, #12469, #12557, #13603, #9743, #1760, #270, #14919, #16250, #4156, #4426, #15270, #13516, #12289, #13685, #184, #16520, #5851, #2812, #6913, #10970, #16339, #16432, #442, #13770, #1671, #4246, #5678, #7085, #9657, #15007, #7170, #1407, #1583, #4334, #354, #7002, #11058, #5761, #9835, #15180, #3082, #7519, #10261, #8854, #14122, #10008 ),
 .UNSPECIFIED., .F., .F.,
 ( 4, 2, 2, 2, 2, 2, 2, 2, 2, 2, 2, 2, 2, 2, 2, 2, 2, 2, 2, 2, 2, 2, 2, 2, 2, 2, 2, 2, 2, 2, 2, 2, 4 ),
 ( 0.000000000000000000, 0.002635407943176078672, 0.005270815886352157344, 0.006588519857940197330, 0.007906223829528238184, 0.01054163177270431989, 0.01185933574429236248, 0.01317703971588040680, 0.01581244765905649372, 0.01713015163064453630, 0.01844785560223257889, 0.01976555957382062148, 0.02108326354540866060, 0.02240096751699670319, 0.02305981950279072101, 0.02371867148858473884, 0.02404809748148175122, 0.02437752347437876013, 0.02470694946727576904, 0.02503637546017278143, 0.02536580145306978687, 0.02569522744596679925, 0.02635407943176082748, 0.02701293141755485919, 0.02767178340334888742, 0.02898948737493693695, 0.03162489531811304294, 0.03294259928970109941, 0.03426030326128915587, 0.03689571120446526187, 0.03821341517605331140, 0.03953111914764136786, 0.04216652709081747386 ),
 .UNSPECIFIED. ) ;
#8841=CARTESIAN_POINT ( 'NONE',  ( 1.561832610794586538E-12, -54.11249999999986926, -18.62500000000000000 ) ) ;
#8842=EDGE_CURVE ( 'NONE', #16308, #9435, #6070, .T. ) ;
#8844=CARTESIAN_POINT ( 'NONE',  ( -7.714727599197335195, -5.203124999999987566, -18.62500000000064304 ) ) ;
#8854=CARTESIAN_POINT ( 'NONE',  ( 11.28538604045423810, -4.913438141674765840E-17, -1.789734987990715620 ) ) ;
#8862=CARTESIAN_POINT ( 'NONE',  ( -4.711679271994915652, -18.69687499999997726, 11.37499999999960210 ) ) ;
#8871=CARTESIAN_POINT ( 'NONE',  ( -11.37500000000039790, -2.115624999999976996, 4.711679271993001628 ) ) ;
#8875=CARTESIAN_POINT ( 'NONE',  ( 18.62499999999934985, -65.55937499999983231, 7.714727599200467800 ) ) ;
#8894=CARTESIAN_POINT ( 'NONE',  ( 13.16986379959834075, -31.21874999999992539, 13.16986379960055231 ) ) ;
#8904=CARTESIAN_POINT ( 'NONE',  ( 11.37500000000000178, -42.69999999999988205, 9.531744055041752924E-13 ) ) ;
#8909=ORIENTED_EDGE ( 'NONE', *, *, #8842, .T. ) ;
#8911=CARTESIAN_POINT ( 'NONE',  ( 4.711679271994911211, -27.02187499999995524, -11.37499999999960210 ) ) ;
#8919=CARTESIAN_POINT ( 'NONE',  ( 18.62500000000064304, -67.64062499999984368, -7.714727599197335195 ) ) ;
#8921=CARTESIAN_POINT ( 'NONE',  ( -1.564113515457998572E-12, -12.48749999999997051, 18.62500000000000000 ) ) ;
#8923=CARTESIAN_POINT ( 'NONE',  ( 1.561832610794586538E-12, -20.81249999999995026, -18.62500000000000000 ) ) ;
#8942=CARTESIAN_POINT ( 'NONE',  ( 8.043339635996298753, -38.46874999999992895, 8.043339635997652337 ) ) ;
#8951=CARTESIAN_POINT ( 'NONE',  ( -1.564113515457998370E-12, -71.83749999999979252, 18.62500000000000000 ) ) ;
#8958=CARTESIAN_POINT ( 'NONE',  ( -13.16986379959834252, -89.49374999999979252, -13.16986379960055054 ) ) ;
#8978=CARTESIAN_POINT ( 'NONE',  ( 18.62499999999935341, -106.1093749999997868, 7.714727599200469577 ) ) ;
#8987=CARTESIAN_POINT ( 'NONE',  ( 9.538709233711902776E-13, -13.56249999999995026, -11.37500000000000178 ) ) ;
#8994=CARTESIAN_POINT ( 'NONE',  ( 11.37500000000000000, -83.24999999999980105, 9.531744055041752924E-13 ) ) ;
#9003=CARTESIAN_POINT ( 'NONE',  ( -18.62500000000000000, -74.92499999999982663, -1.562973063126292555E-12 ) ) ;
#9005=CARTESIAN_POINT ( 'NONE',  ( -18.62499999999934985, -40.58437499999990905, -7.714727599200458918 ) ) ;
#9008=CARTESIAN_POINT ( 'NONE',  ( 18.62500000000000000, -33.29999999999991900, 1.560692158462880521E-12 ) ) ;
#9028=CARTESIAN_POINT ( 'NONE',  ( -11.37500000000039613, -16.61562499999998010, 4.711679271993000739 ) ) ;
#9040=CARTESIAN_POINT ( 'NONE',  ( -8.043339635996304082, -48.94374999999985931, -8.043339635997652337 ) ) ;
#9044=CARTESIAN_POINT ( 'NONE',  ( -13.16986379960055231, -77.00624999999982379, 13.16986379959834252 ) ) ;
#9064=ORIENTED_EDGE ( 'NONE', *, *, #2992, .T. ) ;
#9068=CARTESIAN_POINT ( 'NONE',  ( 18.62500000000000000, -107.1499999999997783, 1.560692158462880521E-12 ) ) ;
#9076=CARTESIAN_POINT ( 'NONE',  ( 7.205550358426942026, -99.99999999999997158, 10.23940715599030327 ) ) ;
#9078=CARTESIAN_POINT ( 'NONE',  ( 9.538709233711902776E-13, -63.51249999999981810, -11.37500000000000178 ) ) ;
#9088=CARTESIAN_POINT ( 'NONE',  ( 11.37500000000039613, -8.290625000000000355, -4.711679271993002516 ) ) ;
#9094=( BOUNDED_CURVE ( )  B_SPLINE_CURVE ( 2, ( #7025, #11081, #4535, #12660, #8614, #12492, #4450, #13966, #3010, #7189, #16455, #10905, #466, #5874, #16274, #15291, #3193, #1863, #7277, #4180, #9592, #2834, #8265, #1518, #3283, #14314, #10028, #10196, #2285, #6047, #16977, #16716, #15549, #12838, #15464, #11513, #15723, #4795, #4622, #15376, #11685, #11429, #7542, #6214, #7457, #8699, #2032, #17061, #3461, #4879, #4965, #14060, #12920, #1945, #7367, #725, #10369, #11601, #4708, #10111, #2201, #13091, #6299, #8875, #10282, #3374, #7627, #16890, #3630, #12747, #16800, #15633, #8787, #14144, #9044, #6134, #14229, #14396, #2114, #803, #13004, #634, #7713, #5959, #11339, #3542, #8958, #887, #10708, #8151, #15988, #5323, #17148, #6564, #14485, #10539, #3892 ),
 .UNSPECIFIED., .F., .F. ) 
 B_SPLINE_CURVE_WITH_KNOTS ( ( 3, 2, 2, 2, 2, 2, 2, 2, 2, 2, 2, 2, 2, 2, 2, 2, 2, 2, 2, 2, 2, 2, 2, 2, 2, 2, 2, 2, 2, 2, 2, 2, 2, 2, 2, 2, 2, 2, 2, 2, 2, 2, 2, 2, 2, 2, 2, 2, 3 ),
 ( 0.000000000000000000, 0.02083333333333333218, 0.04166666666666666435, 0.06250000000000000000, 0.08333333333333332871, 0.1041666666666666713, 0.1250000000000000000, 0.1458333333333333426, 0.1666666666666666574, 0.1875000000000000000, 0.2083333333333333426, 0.2291666666666666574, 0.2500000000000000000, 0.2708333333333333148, 0.2916666666666666852, 0.3125000000000000000, 0.3333333333333333148, 0.3541666666666666852, 0.3750000000000000000, 0.3958333333333333148, 0.4166666666666666852, 0.4375000000000000000, 0.4583333333333333148, 0.4791666666666666852, 0.5000000000000000000, 0.5208333333333333703, 0.5416666666666666297, 0.5625000000000000000, 0.5833333333333333703, 0.6041666666666666297, 0.6250000000000000000, 0.6458333333333333703, 0.6666666666666666297, 0.6875000000000000000, 0.7083333333333333703, 0.7291666666666666297, 0.7500000000000000000, 0.7708333333333333703, 0.7916666666666666297, 0.8125000000000000000, 0.8333333333333333703, 0.8541666666666666297, 0.8750000000000000000, 0.8958333333333333703, 0.9166666666666666297, 0.9375000000000000000, 0.9583333333333333703, 0.9791666666666666297, 1.000000000000000000 ),
 .UNSPECIFIED. ) 
 CURVE ( )  GEOMETRIC_REPRESENTATION_ITEM ( )  RATIONAL_B_SPLINE_CURVE ( ( 1.000000000000000000, 0.9238795325112867385, 1.000000000000000000, 0.9238795325112867385, 1.000000000000000000, 0.9238795325112867385, 1.000000000000000000, 0.9238795325112867385, 1.000000000000000000, 0.9238795325112867385, 1.000000000000000000, 0.9238795325112867385, 1.000000000000000000, 0.9238795325112867385, 1.000000000000000000, 0.9238795325112867385, 1.000000000000000000, 0.9238795325112867385, 1.000000000000000000, 0.9238795325112867385, 1.000000000000000000, 0.9238795325112867385, 1.000000000000000000, 0.9238795325112867385, 1.000000000000000000, 0.9238795325112867385, 1.000000000000000000, 0.9238795325112867385, 1.000000000000000000, 0.9238795325112867385, 1.000000000000000000, 0.9238795325112867385, 1.000000000000000000, 0.9238795325112867385, 1.000000000000000000, 0.9238795325112867385, 1.000000000000000000, 0.9238795325112867385, 1.000000000000000000, 0.9238795325112867385, 1.000000000000000000, 0.9238795325112867385, 1.000000000000000000, 0.9238795325112867385, 1.000000000000000000, 0.9238795325112867385, 1.000000000000000000, 0.9238795325112867385, 1.000000000000000000, 0.9238795325112867385, 1.000000000000000000, 0.9238795325112867385, 1.000000000000000000, 0.9238795325112867385, 1.000000000000000000, 0.9238795325112867385, 1.000000000000000000, 0.9238795325112867385, 1.000000000000000000, 0.9238795325112867385, 1.000000000000000000, 0.9238795325112867385, 1.000000000000000000, 0.9238795325112867385, 1.000000000000000000, 0.9238795325112867385, 1.000000000000000000, 0.9238795325112867385, 1.000000000000000000, 0.9238795325112867385, 1.000000000000000000, 0.9238795325112867385, 1.000000000000000000, 0.9238795325112867385, 1.000000000000000000, 0.9238795325112867385, 1.000000000000000000, 0.9238795325112867385, 1.000000000000000000, 0.9238795325112867385, 1.000000000000000000, 0.9238795325112867385, 1.000000000000000000, 0.9238795325112867385, 1.000000000000000000, 0.9238795325112867385, 1.000000000000000000, 0.9238795325112867385, 1.000000000000000000, 0.9238795325112867385, 1.000000000000000000, 0.9238795325112867385, 1.000000000000000000, 0.9238795325112867385, 1.000000000000000000, 0.9238795325112867385, 1.000000000000000000 ) ) 
 REPRESENTATION_ITEM ( '' )  );
#9097=CARTESIAN_POINT ( 'NONE',  ( -7.714727599200467800, -94.69687499999979252, 18.62499999999934630 ) ) ;
#9099=CARTESIAN_POINT ( 'NONE',  ( -18.62500000000000000, -74.92499999999982663, -1.562973063126292555E-12 ) ) ;
#9102=CARTESIAN_POINT ( 'NONE',  ( 18.62500000000000000, -16.64999999999995950, 1.560692158462880521E-12 ) ) ;
#9122=CARTESIAN_POINT ( 'NONE',  ( -11.37499999999999645, -32.22499999999993747, -9.545674412382054647E-13 ) ) ;
#9132=CARTESIAN_POINT ( 'NONE',  ( 11.37500000000000178, -59.34999999999983800, 9.531744055041752924E-13 ) ) ;
#9159=CARTESIAN_POINT ( 'NONE',  ( -1.564113515457998572E-12, -79.08749999999980673, 18.62500000000000000 ) ) ;
#9168=CARTESIAN_POINT ( 'NONE',  ( -11.37500000000039613, -9.365624999999976552, 4.711679271993002516 ) ) ;
#9169=DIRECTION ( 'NONE',  ( 1.000000000000000000, 0.000000000000000000, 0.000000000000000000 ) ) ;
#9177=CARTESIAN_POINT ( 'NONE',  ( -4.711679271993001628, -62.40312499999986073, -11.37500000000039613 ) ) ;
#9185=CARTESIAN_POINT ( 'NONE',  ( 13.16986379959834075, -81.16874999999980389, 13.16986379960055231 ) ) ;
#9187=CARTESIAN_POINT ( 'NONE',  ( -13.16986379960055231, -93.65624999999977263, 13.16986379959834252 ) ) ;
#9189=CARTESIAN_POINT ( 'NONE',  ( 1.561832610794586538E-12, -70.76249999999983231, -18.62500000000000000 ) ) ;
#9207=CARTESIAN_POINT ( 'NONE',  ( -4.711679271994915652, -35.34687499999993321, 11.37499999999960210 ) ) ;
#9219=CARTESIAN_POINT ( 'NONE',  ( 8.043339635996302306, -73.91874999999977547, 8.043339635997654113 ) ) ;
#9246=CARTESIAN_POINT ( 'NONE',  ( -13.16986379960055231, -43.70624999999989768, 13.16986379959834252 ) ) ;
#9255=CARTESIAN_POINT ( 'NONE',  ( 9.538709233711902776E-13, -20.81249999999995026, -11.37500000000000000 ) ) ;
#9264=CARTESIAN_POINT ( 'NONE',  ( -11.37500000000039613, -83.21562499999981810, 4.711679271993000739 ) ) ;
#9270=CARTESIAN_POINT ( 'NONE',  ( -13.16986379959834252, 1.006250000000015854, -13.16986379960055409 ) ) ;
#9272=CARTESIAN_POINT ( 'NONE',  ( -13.16986379959834252, -15.64374999999994387, -13.16986379960055409 ) ) ;
#9275=CARTESIAN_POINT ( 'NONE',  ( -18.62499999999934985, -73.88437499999982094, -7.714727599200458918 ) ) ;
#9294=CARTESIAN_POINT ( 'NONE',  ( 11.37499999999960210, -89.45937499999983800, 4.711679271994916540 ) ) ;
#9304=CARTESIAN_POINT ( 'NONE',  ( 11.37500000000039613, -60.39062499999985079, -4.711679271993004292 ) ) ;
#9326=CARTESIAN_POINT ( 'NONE',  ( -4.711679271993003404, -5.203124999999986677, -11.37500000000039435 ) ) ;
#9341=CARTESIAN_POINT ( 'NONE',  ( 4.790739404487174724, -100.0000000000000000, 15.33879092982343195 ) ) ;
#9343=CARTESIAN_POINT ( 'NONE',  ( 8.043339635996302306, -73.91874999999977547, 8.043339635997654113 ) ) ;
#9351=CARTESIAN_POINT ( 'NONE',  ( -11.37500000000039613, -49.91562499999989910, 4.711679271993000739 ) ) ;
#9357=CARTESIAN_POINT ( 'NONE',  ( 13.16986379959833897, -57.26874999999984794, 13.16986379960055409 ) ) ;
#9359=CARTESIAN_POINT ( 'NONE',  ( 7.714727599197340524, -6.278124999999967315, 18.62500000000063949 ) ) ;
#9368=CARTESIAN_POINT ( 'NONE',  ( 0.000000000000000000, 0.000000000000000000, 0.000000000000000000 ) ) ;
#9380=CARTESIAN_POINT ( 'NONE',  ( -7.714727599197334307, -29.10312499999994884, -18.62500000000064659 ) ) ;
#9388=CARTESIAN_POINT ( 'NONE',  ( -11.37500000000000178, -51.02499999999986358, -9.545674412382054647E-13 ) ) ;
#9389=CARTESIAN_POINT ( 'NONE',  ( -18.62499999999934985, -40.58437499999990905, -7.714727599200458918 ) ) ;
#9416=CARTESIAN_POINT ( 'NONE',  ( -7.714727599200467800, -44.74687499999989626, 18.62499999999934630 ) ) ;
#9428=CARTESIAN_POINT ( 'NONE',  ( 8.043339635997654113, -35.38124999999991616, -8.043339635996304082 ) ) ;
#9435=VERTEX_POINT ( 'NONE', #6182 ) ;
#9437=CARTESIAN_POINT ( 'NONE',  ( -4.711679271993001628, -95.70312499999977263, -11.37500000000039613 ) ) ;
#9443=CARTESIAN_POINT ( 'NONE',  ( 18.62499999999935341, -25.00937499999992397, 7.714727599200469577 ) ) ;
#9445=CARTESIAN_POINT ( 'NONE',  ( -18.62500000000064659, -2.115624999999976996, 7.714727599197333419 ) ) ;
#9448=CARTESIAN_POINT ( 'NONE',  ( -1.564113515457998572E-12, -95.73749999999976978, 18.62500000000000000 ) ) ;
#9466=CARTESIAN_POINT ( 'NONE',  ( 13.16986379959833897, -21.81874999999996589, 13.16986379960055409 ) ) ;
#9476=CARTESIAN_POINT ( 'NONE',  ( 4.711679271994909435, -53.07187499999987068, -11.37499999999960387 ) ) ;
#9502=CARTESIAN_POINT ( 'NONE',  ( 18.62499999999934630, -48.90937499999989058, 7.714727599200467800 ) ) ;
#9506=DIRECTION ( 'NONE',  ( 0.000000000000000000, 1.000000000000000000, 0.000000000000000000 ) ) ;
#9515=CARTESIAN_POINT ( 'NONE',  ( -8.043339635997654113, -69.75624999999980957, 8.043339635996304082 ) ) ;
#9525=CARTESIAN_POINT ( 'NONE',  ( -11.37499999999960210, -97.78437499999979821, -4.711679271994911211 ) ) ;
#9532=CARTESIAN_POINT ( 'NONE',  ( -7.714727599197334307, -14.60312499999994706, -18.62500000000064659 ) ) ;
#9534=CARTESIAN_POINT ( 'NONE',  ( -18.62500000000064659, -35.41562499999989200, 7.714727599197333419 ) ) ;
#9554=CARTESIAN_POINT ( 'NONE',  ( -18.62499999999935341, -31.18437499999994600, -7.714727599200458030 ) ) ;
#9563=CARTESIAN_POINT ( 'NONE',  ( -18.62500000000000000, -8.324999999999979750, -1.562973063126292555E-12 ) ) ;
#9568=CARTESIAN_POINT ( 'NONE',  ( 18.07672611500867532, 1.677322744816967809E-15, -4.362237117369845762 ) ) ;
#9592=CARTESIAN_POINT ( 'NONE',  ( 1.561832610794586538E-12, -20.81249999999995026, -18.62500000000000000 ) ) ;
#9602=CARTESIAN_POINT ( 'NONE',  ( 18.62040007950909271, -99.99999999999997158, 0.8650468441352018312 ) ) ;
#9604=CARTESIAN_POINT ( 'NONE',  ( -4.711679271994916540, -78.04687499999982947, 11.37499999999960210 ) ) ;
#9612=CARTESIAN_POINT ( 'NONE',  ( -13.16986379960055409, -34.30624999999993463, 13.16986379959834252 ) ) ;
#9620=CARTESIAN_POINT ( 'NONE',  ( -1.564113515457998370E-12, -55.18749999999985079, 18.62500000000000000 ) ) ;
#9622=CARTESIAN_POINT ( 'NONE',  ( 7.714727599200456254, -79.12187499999980389, -18.62499999999935341 ) ) ;
#9631=CARTESIAN_POINT ( 'NONE',  ( 18.62499999999934630, -15.60937499999996270, 7.714727599200467800 ) ) ;
#9642=CARTESIAN_POINT ( 'NONE',  ( -18.62500000000064659, -9.365624999999976552, 7.714727599197335195 ) ) ;
#9644=CARTESIAN_POINT ( 'NONE',  ( 13.16986379960055409, -25.98124999999995310, -13.16986379959834430 ) ) ;
#9657=CARTESIAN_POINT ( 'NONE',  ( 4.460904823772671612, -6.117673133592659619E-13, -12.67084129013523430 ) ) ;
#9690=CARTESIAN_POINT ( 'NONE',  ( 4.711679271993006068, -96.77812499999976126, 11.37500000000039257 ) ) ;
#9701=CARTESIAN_POINT ( 'NONE',  ( -13.16986379960055409, -50.95624999999989768, 13.16986379959834252 ) ) ;
#9708=CARTESIAN_POINT ( 'NONE',  ( 18.62500000000000000, -9.399999999999959499, 1.560692158462880521E-12 ) ) ;
#9710=CARTESIAN_POINT ( 'NONE',  ( 7.714727599200456254, -62.47187499999984084, -18.62499999999935341 ) ) ;
#9730=CARTESIAN_POINT ( 'NONE',  ( -18.62500000000064659, -49.91562499999989910, 7.714727599197333419 ) ) ;
#9743=CARTESIAN_POINT ( 'NONE',  ( 7.564450330115305654, -3.230386817174870386E-14, -15.36044013669110164 ) ) ;
#9759=CARTESIAN_POINT ( 'NONE',  ( 9.538709233711902776E-13, -54.11249999999986926, -11.37500000000000000 ) ) ;
#9778=CARTESIAN_POINT ( 'NONE',  ( 4.711679271993006068, -80.12812499999981242, 11.37500000000039257 ) ) ;
#9788=CARTESIAN_POINT ( 'NONE',  ( 18.62499999999935341, -72.80937499999984652, 7.714727599200469577 ) ) ;
#9797=CARTESIAN_POINT ( 'NONE',  ( 18.62499999999935341, -41.65937499999989058, 7.714727599200469577 ) ) ;
#9803=CARTESIAN_POINT ( 'NONE',  ( 8.043339635997654113, -52.03124999999987921, -8.043339635996304082 ) ) ;
#9820=CARTESIAN_POINT ( 'NONE',  ( -7.714727599197335195, -5.203124999999987566, -18.62500000000064304 ) ) ;
#9823=CARTESIAN_POINT ( 'NONE',  ( 7.714727599197340524, -70.72812499999984936, 18.62500000000063949 ) ) ;
#9835=CARTESIAN_POINT ( 'NONE',  ( 10.01414618136188217, -1.361280322109220638E-15, -6.060987932350863971 ) ) ;
#9850=CARTESIAN_POINT ( 'NONE',  ( 8.043339635996300530, -31.21874999999992539, 8.043339635997654113 ) ) ;
#9867=CARTESIAN_POINT ( 'NONE',  ( 8.043339635997652337, -9.331249999999993605, -8.043339635996302306 ) ) ;
#9876=CARTESIAN_POINT ( 'NONE',  ( 18.62500000000000000, -57.19999999999988916, 1.560692158462880521E-12 ) ) ;
#9885=CARTESIAN_POINT ( 'NONE',  ( -7.714727599200466912, -87.44687499999976410, 18.62499999999935341 ) ) ;
#9893=CARTESIAN_POINT ( 'NONE',  ( -11.37500000000000000, -58.27499999999986358, -9.545674412382054647E-13 ) ) ;
#9909=CARTESIAN_POINT ( 'NONE',  ( 1.561832610794586740E-12, -78.01249999999983231, -18.62500000000000000 ) ) ;
#9921=CARTESIAN_POINT ( 'NONE',  ( 10.83524660546097351, -5.362028352459062835E-15, -14.01674796189367100 ) ) ;
#9935=CARTESIAN_POINT ( 'NONE',  ( 18.62500000000000000, -92.64999999999974989, 1.560692158462880521E-12 ) ) ;
#9936=CARTESIAN_POINT ( 'NONE',  ( 9.538709233711902776E-13, -37.46249999999991331, -11.37500000000000000 ) ) ;
#9962=CARTESIAN_POINT ( 'NONE',  ( -18.62499999999935341, -31.18437499999994600, -7.714727599200458030 ) ) ;
#9970=CARTESIAN_POINT ( 'NONE',  ( 1.561832610794586740E-12, -46.86249999999987637, -18.62500000000000000 ) ) ;
#9979=CARTESIAN_POINT ( 'NONE',  ( -11.37499999999960387, -73.88437499999982094, -4.711679271994910323 ) ) ;
#9995=CARTESIAN_POINT ( 'NONE',  ( 1.561832610794586538E-12, -4.162499999999989875, -18.62500000000000000 ) ) ;
#9996=CARTESIAN_POINT ( 'NONE',  ( 18.62499999999935341, -106.1093749999997868, 7.714727599200469577 ) ) ;
#10008=CARTESIAN_POINT ( 'NONE',  ( 11.37500000000000000, -9.629649721936179265E-32, 9.531744055041752924E-13 ) ) ;
#10022=CARTESIAN_POINT ( 'NONE',  ( 11.37500000000039613, -27.09062499999992113, -4.711679271993004292 ) ) ;
#10023=CARTESIAN_POINT ( 'NONE',  ( 9.538709233711902776E-13, -87.41249999999979536, -11.37500000000000000 ) ) ;
#10028=CARTESIAN_POINT ( 'NONE',  ( -13.16986379960055231, -27.05624999999993463, 13.16986379959834252 ) ) ;
#10049=CARTESIAN_POINT ( 'NONE',  ( -18.62500000000064659, -99.86562499999978115, 7.714727599197333419 ) ) ;
#10057=CARTESIAN_POINT ( 'NONE',  ( 4.711679271994911211, -12.52187499999995524, -11.37499999999960743 ) ) ;
#10066=CARTESIAN_POINT ( 'NONE',  ( -11.37499999999960210, -14.53437499999998295, -4.711679271994911211 ) ) ;
#10080=CARTESIAN_POINT ( 'NONE',  ( -1.564113515457998572E-12, -29.13749999999993179, 18.62500000000000000 ) ) ;
#10082=CARTESIAN_POINT ( 'NONE',  ( 7.714727599200456254, -76.97187499999985505, -18.62499999999935341 ) ) ;
#10107=CARTESIAN_POINT ( 'NONE',  ( -8.043339635997654113, -36.45624999999989768, 8.043339635996304082 ) ) ;
#10108=CARTESIAN_POINT ( 'NONE',  ( 8.043339635997654113, -68.68124999999983515, -8.043339635996304082 ) ) ;
#10111=CARTESIAN_POINT ( 'NONE',  ( -7.714727599200466912, -61.39687499999985221, 18.62499999999934985 ) ) ;
#10131=CARTESIAN_POINT ( 'NONE',  ( 7.714727599197338748, -13.52812499999996732, 18.62500000000063949 ) ) ;
#10141=CARTESIAN_POINT ( 'NONE',  ( -8.043339635996304082, -32.29374999999990337, -8.043339635997652337 ) ) ;
#10150=CARTESIAN_POINT ( 'NONE',  ( 8.043339635996298753, -21.81874999999996234, 8.043339635997652337 ) ) ;
#10166=CARTESIAN_POINT ( 'NONE',  ( -7.714727599200467800, -11.44687499999997371, 18.62499999999934630 ) ) ;
#10168=CARTESIAN_POINT ( 'NONE',  ( -7.714727599197335195, -38.50312499999991189, -18.62500000000064304 ) ) ;
#10183=CARTESIAN_POINT ( 'NONE',  ( 8.043339635996298753, -21.81874999999996234, 8.043339635997652337 ) ) ;
#10191=CARTESIAN_POINT ( 'NONE',  ( 7.714727599197340524, -89.52812499999977547, 18.62500000000063949 ) ) ;
#10196=CARTESIAN_POINT ( 'NONE',  ( -7.714727599200466912, -28.09687499999992966, 18.62499999999934985 ) ) ;
#10216=CARTESIAN_POINT ( 'NONE',  ( 7.714727599197338748, -30.17812499999993747, 18.62500000000063949 ) ) ;
#10225=CARTESIAN_POINT ( 'NONE',  ( -11.37500000000000178, -34.37499999999990052, -9.545674412382054647E-13 ) ) ;
#10234=CARTESIAN_POINT ( 'NONE',  ( -11.37500000000039613, -33.26562499999994316, 4.711679271993000739 ) ) ;
#10244=CARTESIAN_POINT ( 'NONE',  ( 11.37500000000000000, -99.89999999999976410, 0.000000000000000000 ) ) ;
#10245=CARTESIAN_POINT ( 'NONE',  ( -7.714727599200467800, -61.39687499999984510, 18.62499999999934630 ) ) ;
#10247=CARTESIAN_POINT ( 'NONE',  ( -13.16986379960055231, -27.05624999999993463, 13.16986379959834252 ) ) ;
#10249=CARTESIAN_POINT ( 'NONE',  ( -7.714727599200467800, -11.44687499999997371, 18.62499999999934630 ) ) ;
#10261=CARTESIAN_POINT ( 'NONE',  ( 11.02516507505776211, -4.913438141677136737E-17, -3.106252184828564467 ) ) ;
#10267=CARTESIAN_POINT ( 'NONE',  ( 11.37499999999999645, -23.89999999999996305, 9.531744055041752924E-13 ) ) ;
#10277=CARTESIAN_POINT ( 'NONE',  ( 18.62500000000000000, -75.99999999999980105, 1.560692158462880521E-12 ) ) ;
#10282=CARTESIAN_POINT ( 'NONE',  ( 18.62500000000000000, -66.59999999999983800, 1.560692158462880521E-12 ) ) ;
#10301=CARTESIAN_POINT ( 'NONE',  ( 7.714727599197340524, -104.0281249999997755, 18.62500000000063949 ) ) ;
#10311=CARTESIAN_POINT ( 'NONE',  ( -8.043339635997654113, -36.45624999999989768, 8.043339635996304082 ) ) ;
#10318=CARTESIAN_POINT ( 'NONE',  ( -4.711679271994915652, -35.34687499999993321, 11.37499999999960210 ) ) ;
#10330=CARTESIAN_POINT ( 'NONE',  ( 7.714727599200458030, -69.72187499999982663, -18.62499999999934985 ) ) ;
#10332=CARTESIAN_POINT ( 'NONE',  ( -7.714727599197335195, -71.80312499999982379, -18.62500000000064304 ) ) ;
#10334=CARTESIAN_POINT ( 'NONE',  ( -18.62500000000000000, -58.27499999999986358, -1.562973063126292555E-12 ) ) ;
#10356=CARTESIAN_POINT ( 'NONE',  ( -9.552639591052204498E-13, -69.68749999999984368, 11.37499999999999645 ) ) ;
#10365=CARTESIAN_POINT ( 'NONE',  ( -9.552639591052204498E-13, -55.18749999999985079, 11.37500000000000178 ) ) ;
#10369=CARTESIAN_POINT ( 'NONE',  ( -18.62500000000000000, -58.27499999999986358, -1.562973063126292555E-12 ) ) ;
#10391=CARTESIAN_POINT ( 'NONE',  ( -13.16986379959834252, -22.89374999999994387, -13.16986379960055054 ) ) ;
#10397=CARTESIAN_POINT ( 'NONE',  ( 11.30201554348636783, -99.99999999999994316, 1.743143577145335854 ) ) ;
#10399=CARTESIAN_POINT ( 'NONE',  ( 4.711679271993006957, -56.22812499999984936, 11.37500000000039613 ) ) ;
#10407=CARTESIAN_POINT ( 'NONE',  ( 8.043339635997652337, -9.331249999999993605, -8.043339635996302306 ) ) ;
#10415=CARTESIAN_POINT ( 'NONE',  ( -13.16986379960055231, -60.35624999999985363, 13.16986379959834252 ) ) ;
#10417=CARTESIAN_POINT ( 'NONE',  ( 18.62500000000000000, -16.64999999999995950, 1.560692158462880521E-12 ) ) ;
#10420=CARTESIAN_POINT ( 'NONE',  ( -13.16986379959834252, -56.19374999999985931, -13.16986379960055054 ) ) ;
#10441=CARTESIAN_POINT ( 'NONE',  ( -11.37499999999960210, -64.48437499999987210, -4.711679271994911211 ) ) ;
#10451=CARTESIAN_POINT ( 'NONE',  ( -11.37500000000039790, -68.71562499999981810, 4.711679271993001628 ) ) ;
#10484=CARTESIAN_POINT ( 'NONE',  ( 11.38173386846534108, -99.99999999999998579, 0.8785756797233987836 ) ) ;
#10486=CARTESIAN_POINT ( 'NONE',  ( 11.37500000000000000, 4.439344646909156023E-16, 9.531744055041752924E-13 ) ) ;
#10495=CARTESIAN_POINT ( 'NONE',  ( 11.37499999999960210, -106.1093749999997584, 4.711679271994916540 ) ) ;
#10502=CARTESIAN_POINT ( 'NONE',  ( -18.62500000000064659, -75.96562499999980389, 7.714727599197335195 ) ) ;
#10505=CARTESIAN_POINT ( 'NONE',  ( 13.16986379960055409, 5.168750000000006395, -13.16986379959834430 ) ) ;
#10508=CARTESIAN_POINT ( 'NONE',  ( -13.16986379960055231, -27.05624999999993463, 13.16986379959834252 ) ) ;
#10524=CARTESIAN_POINT ( 'NONE',  ( 8.043339635996298753, -55.11874999999988489, 8.043339635997652337 ) ) ;
#10535=CARTESIAN_POINT ( 'NONE',  ( 11.37500000000039613, -77.04062499999979252, -4.711679271993004292 ) ) ;
#10539=CARTESIAN_POINT ( 'NONE',  ( 18.62499999999934985, -98.85937499999975842, 7.714727599200467800 ) ) ;
#10563=CARTESIAN_POINT ( 'NONE',  ( 18.62500000000000000, -49.94999999999988205, 1.560692158462880521E-12 ) ) ;
#10570=CARTESIAN_POINT ( 'NONE',  ( 4.269545073161230775, -100.0000000000000284, 13.16816258391341421 ) ) ;
#10572=CARTESIAN_POINT ( 'NONE',  ( -9.552639591052204498E-13, -29.13749999999993179, 11.37500000000000000 ) ) ;
#10580=CARTESIAN_POINT ( 'NONE',  ( -7.714727599197334307, -12.45312499999998757, -18.62500000000064659 ) ) ;
#10588=CARTESIAN_POINT ( 'NONE',  ( -1.564113515457998572E-12, -79.08749999999980673, 18.62500000000000000 ) ) ;
#10590=CARTESIAN_POINT ( 'NONE',  ( -13.16986379960055409, -19.80624999999993463, 13.16986379959834252 ) ) ;
#10608=CARTESIAN_POINT ( 'NONE',  ( 7.714727599200456254, -43.67187499999991473, -18.62499999999935341 ) ) ;
#10617=CARTESIAN_POINT ( 'NONE',  ( -4.711679271993003404, -64.55312499999983800, -11.37500000000039613 ) ) ;
#10618=CARTESIAN_POINT ( 'NONE',  ( -13.16986379960055231, -10.40624999999997513, 13.16986379959834252 ) ) ;
#10644=CARTESIAN_POINT ( 'NONE',  ( -18.62500000000000000, -58.27499999999986358, -1.562973063126292555E-12 ) ) ;
#10654=CARTESIAN_POINT ( 'NONE',  ( 15.00421320149717097, -100.0000000000000000, 10.33632056195987481 ) ) ;
#10656=CARTESIAN_POINT ( 'NONE',  ( -8.043339635997654113, -27.05624999999993463, 8.043339635996302306 ) ) ;
#10664=CARTESIAN_POINT ( 'NONE',  ( -9.552639591052204498E-13, -53.03749999999988773, 11.37499999999999645 ) ) ;
#10670=CARTESIAN_POINT ( 'NONE',  ( -7.714727599197334307, -47.90312499999986784, -18.62500000000064659 ) ) ;
#10672=CARTESIAN_POINT ( 'NONE',  ( 13.16986379960055409, -11.48124999999995488, -13.16986379959834430 ) ) ;
#10675=CARTESIAN_POINT ( 'NONE',  ( 7.714727599197338748, -80.12812499999981242, 18.62500000000063949 ) ) ;
#10694=CARTESIAN_POINT ( 'NONE',  ( -7.714727599200466912, -18.69687499999997726, 18.62499999999935341 ) ) ;
#10702=CARTESIAN_POINT ( 'NONE',  ( 4.711679271993006957, -72.87812499999979821, 11.37500000000039613 ) ) ;
#10703=CARTESIAN_POINT ( 'NONE',  ( -13.16986379959834252, -39.54374999999990337, -13.16986379960055054 ) ) ;
#10705=CARTESIAN_POINT ( 'NONE',  ( 11.37637957285810586, -100.0000000000000000, 0.000000000000000000 ) ) ;
#10708=CARTESIAN_POINT ( 'NONE',  ( -18.62500000000000000, -91.57499999999977547, -1.562973063126292555E-12 ) ) ;
#10727=CARTESIAN_POINT ( 'NONE',  ( 13.16986379960055054, -52.03124999999987921, -13.16986379959834430 ) ) ;
#10731=PLANE ( 'NONE',  #12198 ) ;
#10736=PRODUCT_DEFINITION_CONTEXT ( 'detailed design', #2336, 'design' ) ;
#10738=CARTESIAN_POINT ( 'NONE',  ( 17.54501034274306193, -99.99999999999994316, 5.877963988053037880 ) ) ;
#10740=CARTESIAN_POINT ( 'NONE',  ( 11.37500000000039435, -1.040624999999997025, -4.711679271993004292 ) ) ;
#10748=CARTESIAN_POINT ( 'NONE',  ( 1.561832610794586740E-12, -11.41249999999999254, -18.62500000000000000 ) ) ;
#10754=CARTESIAN_POINT ( 'NONE',  ( -18.62499999999935341, -33.33437499999990195, -7.714727599200458030 ) ) ;
#10757=CARTESIAN_POINT ( 'NONE',  ( -7.714727599197335195, -88.45312499999978684, -18.62500000000064304 ) ) ;
#10760=CARTESIAN_POINT ( 'NONE',  ( 7.714727599200458030, -86.37187499999978968, -18.62499999999934985 ) ) ;
#10778=CARTESIAN_POINT ( 'NONE',  ( -1.564113515457998370E-12, -36.38749999999993179, 18.62500000000000000 ) ) ;
#10786=CARTESIAN_POINT ( 'NONE',  ( 4.711679271994909435, -19.77187499999995168, -11.37499999999960387 ) ) ;
#10787=CARTESIAN_POINT ( 'NONE',  ( 7.714727599197338748, -30.17812499999993747, 18.62500000000063949 ) ) ;
#10809=CARTESIAN_POINT ( 'NONE',  ( -4.711679271994915652, -11.44687499999997371, 11.37499999999960210 ) ) ;
#10813=CARTESIAN_POINT ( 'NONE',  ( 1.561832610794586538E-12, -54.11249999999986926, -18.62500000000000000 ) ) ;
#10826=CARTESIAN_POINT ( 'NONE',  ( -8.043339635997654113, -86.40624999999977263, 8.043339635996304082 ) ) ;
#10835=CARTESIAN_POINT ( 'NONE',  ( 11.37500000000039613, -58.24062499999988063, -4.711679271993002516 ) ) ;
#10840=CARTESIAN_POINT ( 'NONE',  ( -7.714727599200466912, -54.14687499999985931, 18.62499999999935341 ) ) ;
#10842=CARTESIAN_POINT ( 'NONE',  ( 7.714727599197340524, -22.92812499999992326, 18.62500000000063949 ) ) ;
#10854=EDGE_CURVE ( 'NONE', #2583, #7126, #16959, .T. ) ;
#10864=CARTESIAN_POINT ( 'NONE',  ( 7.714727599200456254, -27.02187499999995524, -18.62499999999935341 ) ) ;
#10873=CARTESIAN_POINT ( 'NONE',  ( -4.711679271994916540, -11.44687499999997371, 11.37499999999960210 ) ) ;
#10874=CARTESIAN_POINT ( 'NONE',  ( 13.16986379959834075, -14.56874999999996589, 13.16986379960055231 ) ) ;
#10880=CARTESIAN_POINT ( 'NONE',  ( 12.99792880889490121, -5.025561147605685224E-16, -12.49106143210709696 ) ) ;
#10905=CARTESIAN_POINT ( 'NONE',  ( -7.714727599200466912, -11.44687499999997371, 18.62499999999934985 ) ) ;
#10913=CARTESIAN_POINT ( 'NONE',  ( 3.629376248049960729, -100.0000000000000711, 14.61214224149137841 ) ) ;
#10915=CARTESIAN_POINT ( 'NONE',  ( 8.043339635996300530, -47.86874999999988489, 8.043339635997654113 ) ) ;
#10926=CARTESIAN_POINT ( 'NONE',  ( 13.16986379959833897, -21.81874999999996589, 13.16986379960055409 ) ) ;
#10933=CARTESIAN_POINT ( 'NONE',  ( -18.62500000000000000, -67.67499999999981242, -1.562973063126292757E-12 ) ) ;
#10935=CARTESIAN_POINT ( 'NONE',  ( -1.564113515457998370E-12, -38.53749999999988063, 18.62500000000000000 ) ) ;
#10958=CARTESIAN_POINT ( 'NONE',  ( -13.16986379960055409, -34.30624999999993463, 13.16986379959834252 ) ) ;
#10964=DIRECTION ( 'NONE',  ( -8.379555213223520053E-14, 0.000000000000000000, 1.000000000000000000 ) ) ;
#10970=CARTESIAN_POINT ( 'NONE',  ( 3.055286883508066875, 9.636628673746404573E-15, -14.49864048043250797 ) ) ;
#11002=CARTESIAN_POINT ( 'NONE',  ( 18.08535795341810726, -99.99999999999998579, 4.251752263608082671 ) ) ;
#11004=CARTESIAN_POINT ( 'NONE',  ( -11.37500000000039613, -75.96562499999980389, 4.711679271993002516 ) ) ;
#11014=CARTESIAN_POINT ( 'NONE',  ( -18.62499999999935341, -64.48437499999987210, -7.714727599200458030 ) ) ;
#11021=CARTESIAN_POINT ( 'NONE',  ( 18.62500000000000000, -26.04999999999992255, 1.560692158462880521E-12 ) ) ;
#11023=CARTESIAN_POINT ( 'NONE',  ( 18.62500000000064659, -43.74062499999988773, -7.714727599197336083 ) ) ;
#11046=CARTESIAN_POINT ( 'NONE',  ( 13.16986379959833897, -55.11874999999988489, 13.16986379960055409 ) ) ;
#11058=CARTESIAN_POINT ( 'NONE',  ( 8.887463110696979030, -7.486575357575272229E-16, -7.985952341615979222 ) ) ;
#11074=CARTESIAN_POINT ( 'NONE',  ( -11.37500000000039613, -75.96562499999981810, 4.711679271993001628 ) ) ;
#11081=CARTESIAN_POINT ( 'NONE',  ( 18.62500000000064304, -1.040624999999997469, -7.714727599197334307 ) ) ;
#11093=CARTESIAN_POINT ( 'NONE',  ( 4.711679271994909435, -53.07187499999987068, -11.37499999999960387 ) ) ;
#11101=CARTESIAN_POINT ( 'NONE',  ( 13.16986379959833897, -55.11874999999988489, 13.16986379960055409 ) ) ;
#11109=CARTESIAN_POINT ( 'NONE',  ( -13.16986379959834252, -48.94374999999985931, -13.16986379960055409 ) ) ;
#11134=CARTESIAN_POINT ( 'NONE',  ( -7.714727599200466912, -85.29687499999984368, 18.62499999999935341 ) ) ;
#11144=CARTESIAN_POINT ( 'NONE',  ( 17.16739154622002062, 3.710240846040480518E-14, -6.862782679473228065 ) ) ;
#11161=CARTESIAN_POINT ( 'NONE',  ( -8.043339635997654113, -60.35624999999985363, 8.043339635996302306 ) ) ;
#11180=CARTESIAN_POINT ( 'NONE',  ( 11.37500000000039435, -84.29062499999983515, -4.711679271993004292 ) ) ;
#11190=CARTESIAN_POINT ( 'NONE',  ( 13.16986379960055409, -75.93124999999983515, -13.16986379959834430 ) ) ;
#11195=AXIS2_PLACEMENT_3D ( 'NONE', #12733, #8773, #2993 ) ;
#11198=CARTESIAN_POINT ( 'NONE',  ( -7.714727599200466912, -37.49687499999989626, 18.62499999999935341 ) ) ;
#11204=CARTESIAN_POINT ( 'NONE',  ( 8.043339635997654113, -68.68124999999983515, -8.043339635996304082 ) ) ;
#11218=CARTESIAN_POINT ( 'NONE',  ( 13.16986379960055054, -2.081249999999994937, -13.16986379959834430 ) ) ;
#11220=CARTESIAN_POINT ( 'NONE',  ( -18.62499999999935341, -97.78437499999979821, -7.714727599200458030 ) ) ;
#11223=ADVANCED_FACE ( 'NONE', ( #2718 ), #16496, .F. ) ;
#11233=CARTESIAN_POINT ( 'NONE',  ( 12.31824352683052304, -2.318222727469660658E-13, -13.04685550568140329 ) ) ;
#11246=CARTESIAN_POINT ( 'NONE',  ( 11.37500000000039613, 6.209375000000004974, -4.711679271993004292 ) ) ;
#11247=CARTESIAN_POINT ( 'NONE',  ( -4.711679271994915652, -78.04687499999982947, 11.37499999999960210 ) ) ;
#11273=CARTESIAN_POINT ( 'NONE',  ( 18.62499999999935341, -39.50937499999993463, 7.714727599200469577 ) ) ;
#11280=CARTESIAN_POINT ( 'NONE',  ( -4.711679271993003404, 2.046875000000014211, -11.37500000000039613 ) ) ;
#11287=CARTESIAN_POINT ( 'NONE',  ( -4.711679271994916540, -44.74687499999989626, 11.37499999999960210 ) ) ;
#11304=CARTESIAN_POINT ( 'NONE',  ( 13.16986379959833897, -105.0687499999997527, 13.16986379960055409 ) ) ;
#11332=CARTESIAN_POINT ( 'NONE',  ( 4.711679271993006957, -22.92812499999992326, 11.37500000000039613 ) ) ;
#11333=CARTESIAN_POINT ( 'NONE',  ( -4.711679271994915652, -44.74687499999989626, 11.37499999999960210 ) ) ;
#11339=CARTESIAN_POINT ( 'NONE',  ( 1.561832610794586538E-12, -87.41249999999979536, -18.62500000000000000 ) ) ;
#11362=CARTESIAN_POINT ( 'NONE',  ( -7.714727599200466912, -85.29687499999984368, 18.62499999999935341 ) ) ;
#11371=CARTESIAN_POINT ( 'NONE',  ( 4.711679271993006957, -22.92812499999992326, 11.37500000000039613 ) ) ;
#11379=CARTESIAN_POINT ( 'NONE',  ( -11.37500000000039613, -42.66562499999989200, 4.711679271993002516 ) ) ;
#11395=CARTESIAN_POINT ( 'NONE',  ( 18.62500000000000000, 0.000000000000000000, 1.560692158462880521E-12 ) ) ;
#11397=CARTESIAN_POINT ( 'NONE',  ( 18.62500000000064304, -1.040624999999997469, -7.714727599197335195 ) ) ;
#11405=UNCERTAINTY_MEASURE_WITH_UNIT (LENGTH_MEASURE( 1.000000000000000082E-05 ), #529, 'distance_accuracy_value', 'NONE');
#11424=CARTESIAN_POINT ( 'NONE',  ( -8.043339635996304082, -15.64374999999994387, -8.043339635997652337 ) ) ;
#11425=CARTESIAN_POINT ( 'NONE',  ( -11.37500000000000000, -58.27499999999986358, -9.545674412382054647E-13 ) ) ;
#11429=CARTESIAN_POINT ( 'NONE',  ( -18.62500000000064659, -42.66562499999989200, 7.714727599197333419 ) ) ;
#11449=CARTESIAN_POINT ( 'NONE',  ( 13.16986379960055409, -92.58124999999979821, -13.16986379959834430 ) ) ;
#11457=CARTESIAN_POINT ( 'NONE',  ( -9.552639591052204498E-13, -38.53749999999988063, 11.37500000000000178 ) ) ;
#11466=CARTESIAN_POINT ( 'NONE',  ( 4.711679271993006068, -80.12812499999981242, 11.37500000000039257 ) ) ;
#11482=CARTESIAN_POINT ( 'NONE',  ( 7.714727599197338748, -46.82812499999989342, 18.62500000000063949 ) ) ;
#11484=CARTESIAN_POINT ( 'NONE',  ( 13.16986379960055054, -35.38124999999991616, -13.16986379959834430 ) ) ;
#11499=CARTESIAN_POINT ( 'NONE',  ( 11.37500000000039435, -50.99062499999987352, -4.711679271993004292 ) ) ;
#11508=CARTESIAN_POINT ( 'NONE',  ( -11.37500000000000178, -1.074999999999978639, -9.545674412382054647E-13 ) ) ;
#11513=CARTESIAN_POINT ( 'NONE',  ( 7.714727599200458030, -36.42187499999990763, -18.62499999999935341 ) ) ;
#11515=DIRECTION ( 'NONE',  ( 0.000000000000000000, 0.000000000000000000, 1.000000000000000000 ) ) ;
#11533=CARTESIAN_POINT ( 'NONE',  ( -18.62500000000064659, -83.21562499999981810, 7.714727599197333419 ) ) ;
#11544=CARTESIAN_POINT ( 'NONE',  ( 4.711679271993006957, -6.278124999999967315, 11.37500000000039613 ) ) ;
#11551=CARTESIAN_POINT ( 'NONE',  ( 11.37500000000039435, -84.29062499999983515, -4.711679271993004292 ) ) ;
#11565=CARTESIAN_POINT ( 'NONE',  ( -18.62499999999934985, -90.53437499999978400, -7.714727599200458918 ) ) ;
#11567=CARTESIAN_POINT ( 'NONE',  ( 7.714727599200458030, -36.42187499999990763, -18.62499999999934985 ) ) ;
#11569=CARTESIAN_POINT ( 'NONE',  ( -1.564113515457998572E-12, -12.48749999999997051, 18.62500000000000000 ) ) ;
#11586=CARTESIAN_POINT ( 'NONE',  ( 11.37499999999960210, -39.50937499999993463, 4.711679271994916540 ) ) ;
#11595=CARTESIAN_POINT ( 'NONE',  ( 4.711679271994911211, -29.17187499999991118, -11.37499999999960743 ) ) ;
#11601=CARTESIAN_POINT ( 'NONE',  ( -18.62500000000064659, -59.31562499999985505, 7.714727599197333419 ) ) ;
#11621=CARTESIAN_POINT ( 'NONE',  ( -18.62500000000000000, -98.82499999999978968, -1.562973063126292757E-12 ) ) ;
#11630=CARTESIAN_POINT ( 'NONE',  ( -8.043339635997654113, -53.10624999999986073, 8.043339635996304082 ) ) ;
#11637=CARTESIAN_POINT ( 'NONE',  ( 4.711679271994911211, -10.37187499999999396, -11.37499999999960210 ) ) ;
#11648=CARTESIAN_POINT ( 'NONE',  ( 13.16986379960055054, -52.03124999999987921, -13.16986379959834430 ) ) ;
#11650=CARTESIAN_POINT ( 'NONE',  ( 18.62500000000000000, -66.59999999999983800, 1.560692158462880521E-12 ) ) ;
#11652=CARTESIAN_POINT ( 'NONE',  ( 7.714727599200458030, -53.07187499999987068, -18.62499999999934985 ) ) ;
#11667=SHAPE_REPRESENTATION_RELATIONSHIP ( 'NONE' , 'NONE' ,  #4322, #11777 ) ;
#11672=CARTESIAN_POINT ( 'NONE',  ( -11.37499999999999645, -65.52499999999986358, -9.545674412382054647E-13 ) ) ;
#11681=CARTESIAN_POINT ( 'NONE',  ( 11.37499999999960565, -91.60937499999975842, 4.711679271994918317 ) ) ;
#11685=CARTESIAN_POINT ( 'NONE',  ( -18.62500000000000000, -41.62499999999990052, -1.562973063126292555E-12 ) ) ;
#11707=CARTESIAN_POINT ( 'NONE',  ( -7.714727599200466912, -101.9468749999998067, 18.62499999999935341 ) ) ;
#11718=CARTESIAN_POINT ( 'NONE',  ( 8.043339635997652337, -28.13124999999991260, -8.043339635996304082 ) ) ;
#11725=CARTESIAN_POINT ( 'NONE',  ( 4.711679271993006957, -37.42812499999992326, 11.37500000000039257 ) ) ;
#11733=CARTESIAN_POINT ( 'NONE',  ( 18.62500000000000000, 7.250000000000001776, 1.560692158462880521E-12 ) ) ;
#11735=CARTESIAN_POINT ( 'NONE',  ( -13.16986379959834252, -56.19374999999985931, -13.16986379960055054 ) ) ;
#11738=CARTESIAN_POINT ( 'NONE',  ( -1.564113515457998572E-12, -29.13749999999993179, 18.62500000000000000 ) ) ;
#11758=CARTESIAN_POINT ( 'NONE',  ( 8.043339635997652337, -75.93124999999983515, -8.043339635996302306 ) ) ;
#11768=CARTESIAN_POINT ( 'NONE',  ( 9.538709233711902776E-13, -46.86249999999987637, -11.37500000000000178 ) ) ;
#11769=CARTESIAN_POINT ( 'NONE',  ( -4.711679271994915652, -94.69687499999976410, 11.37499999999960210 ) ) ;
#11777=ADVANCED_BREP_SHAPE_REPRESENTATION ( '', ( #3202, #16654 ), #7660 ) ;
#11796=CARTESIAN_POINT ( 'NONE',  ( -18.62500000000000000, -91.57499999999977547, -1.562973063126292555E-12 ) ) ;
#11805=CARTESIAN_POINT ( 'NONE',  ( -4.711679271993003404, -81.20312499999978684, -11.37500000000039613 ) ) ;
#11816=CARTESIAN_POINT ( 'NONE',  ( -9.552639591052204498E-13, -19.73749999999997229, 11.37499999999999645 ) ) ;
#11822=CARTESIAN_POINT ( 'NONE',  ( -18.62500000000064659, -2.115624999999976996, 7.714727599197333419 ) ) ;
#11824=CARTESIAN_POINT ( 'NONE',  ( -18.62500000000064659, -26.01562499999994671, 7.714727599197335195 ) ) ;
#11828=CARTESIAN_POINT ( 'NONE',  ( -13.16986379960055231, -10.40624999999997513, 13.16986379959834252 ) ) ;
#11848=CARTESIAN_POINT ( 'NONE',  ( 8.043339635997652337, -59.28124999999987921, -8.043339635996302306 ) ) ;
#11858=CARTESIAN_POINT ( 'NONE',  ( 11.37499999999960565, -41.65937499999989058, 4.711679271994918317 ) ) ;
#11884=CARTESIAN_POINT ( 'NONE',  ( 7.714727599197338748, -46.82812499999989342, 18.62500000000063949 ) ) ;
#11893=CARTESIAN_POINT ( 'NONE',  ( 4.711679271993006957, -72.87812499999979821, 11.37500000000039613 ) ) ;
#11901=CARTESIAN_POINT ( 'NONE',  ( 8.043339635997652337, -59.28124999999987921, -8.043339635996302306 ) ) ;
#11907=CARTESIAN_POINT ( 'NONE',  ( 18.62499999999934630, -98.85937499999975842, 7.714727599200467800 ) ) ;
#11909=CARTESIAN_POINT ( 'NONE',  ( -18.62500000000064659, -18.76562499999993605, 7.714727599197333419 ) ) ;
#11912=CARTESIAN_POINT ( 'NONE',  ( 18.62499999999934630, -98.85937499999975842, 7.714727599200467800 ) ) ;
#11928=CARTESIAN_POINT ( 'NONE',  ( -9.552639591052204498E-13, -53.03749999999988773, 11.37499999999999645 ) ) ;
#11929=ADVANCED_FACE ( 'NONE', ( #5124 ), #15790, .T. ) ;
#11935=EDGE_LOOP ( 'NONE', ( #7019, #9064 ) ) ;
#11939=CARTESIAN_POINT ( 'NONE',  ( 4.711679271994911211, -45.82187499999987779, -11.37499999999960743 ) ) ;
#11940=CARTESIAN_POINT ( 'NONE',  ( 18.62500000000000000, 0.000000000000000000, 1.560692158462880521E-12 ) ) ;
#11967=CARTESIAN_POINT ( 'NONE',  ( 7.714727599200458030, -53.07187499999987068, -18.62499999999934985 ) ) ;
#11976=CARTESIAN_POINT ( 'NONE',  ( 9.538709233711902776E-13, -37.46249999999991331, -11.37500000000000000 ) ) ;
#11977=ADVANCED_FACE ( 'NONE', ( #2745 ), #10731, .F. ) ;
#11986=CARTESIAN_POINT ( 'NONE',  ( -8.043339635997652337, -50.95624999999989768, 8.043339635996300530 ) ) ;
#11992=CARTESIAN_POINT ( 'NONE',  ( -18.62499999999935341, -66.63437499999983515, -7.714727599200458030 ) ) ;
#11994=CARTESIAN_POINT ( 'NONE',  ( -7.714727599200467800, -94.69687499999979252, 18.62499999999934630 ) ) ;
#12015=CARTESIAN_POINT ( 'NONE',  ( 7.714727599200456254, -10.37187499999999396, -18.62499999999935341 ) ) ;
#12024=CARTESIAN_POINT ( 'NONE',  ( 9.538709233711902776E-13, -80.16249999999979536, -11.37500000000000178 ) ) ;
#12025=CARTESIAN_POINT ( 'NONE',  ( -7.714727599197335195, -5.203124999999987566, -18.62500000000064304 ) ) ;
#12060=CARTESIAN_POINT ( 'NONE',  ( 5.656292974072647972, -100.0000000000000000, 15.42281920893911895 ) ) ;
#12062=CARTESIAN_POINT ( 'NONE',  ( 11.37500000000039435, -34.34062499999991047, -4.711679271993004292 ) ) ;
#12070=CARTESIAN_POINT ( 'NONE',  ( 11.37500000000039613, -91.54062499999980673, -4.711679271993002516 ) ) ;
#12075=CARTESIAN_POINT ( 'NONE',  ( 7.714727599197340524, -6.278124999999967315, 18.62500000000063949 ) ) ;
#12077=CARTESIAN_POINT ( 'NONE',  ( -18.62499999999935341, -16.68437499999993889, -7.714727599200458030 ) ) ;
#12097=CARTESIAN_POINT ( 'NONE',  ( 18.62500000000000000, -23.89999999999996305, 1.560692158462880521E-12 ) ) ;
#12106=CARTESIAN_POINT ( 'NONE',  ( -8.043339635996302306, -22.89374999999994387, -8.043339635997654113 ) ) ;
#12107=CARTESIAN_POINT ( 'NONE',  ( -13.16986379959834252, -22.89374999999994387, -13.16986379960055054 ) ) ;
#12132=CARTESIAN_POINT ( 'NONE',  ( 7.714727599200458030, -69.72187499999982663, -18.62499999999934985 ) ) ;
#12144=CARTESIAN_POINT ( 'NONE',  ( -11.37500000000000000, -8.324999999999979750, -9.545674412382054647E-13 ) ) ;
#12155=CARTESIAN_POINT ( 'NONE',  ( 4.711679271993006957, -87.37812499999982663, 11.37500000000039257 ) ) ;
#12161=CARTESIAN_POINT ( 'NONE',  ( -18.62500000000064659, -18.76562499999993605, 7.714727599197333419 ) ) ;
#12164=CARTESIAN_POINT ( 'NONE',  ( 18.62500000000000000, -99.89999999999976410, 1.560692158462880521E-12 ) ) ;
#12172=EDGE_LOOP ( 'NONE', ( #14699, #8192 ) ) ;
#12185=CARTESIAN_POINT ( 'NONE',  ( -9.552639591052204498E-13, -86.33749999999982094, 11.37499999999999645 ) ) ;
#12194=CARTESIAN_POINT ( 'NONE',  ( -8.043339635997654113, -43.70624999999989768, 8.043339635996302306 ) ) ;
#12195=CARTESIAN_POINT ( 'NONE',  ( -7.714727599197335195, -38.50312499999991189, -18.62500000000064304 ) ) ;
#12198=AXIS2_PLACEMENT_3D ( 'NONE', #3586, #9506, #17021 ) ;
#12201=CARTESIAN_POINT ( 'NONE',  ( 16.98133590665164760, 1.089405092048506085E-13, -7.261809523205409178 ) ) ;
#12214=CARTESIAN_POINT ( 'NONE',  ( 9.538709233711902776E-13, -4.162499999999988987, -11.37500000000000000 ) ) ;
#12232=CARTESIAN_POINT ( 'NONE',  ( 13.22006015585995797, -99.99999999999995737, 12.20452656438226846 ) ) ;
#12234=CARTESIAN_POINT ( 'NONE',  ( 9.538709233711902776E-13, -54.11249999999986926, -11.37500000000000000 ) ) ;
#12243=CARTESIAN_POINT ( 'NONE',  ( -4.711679271994915652, -68.64687499999988063, 11.37499999999960210 ) ) ;
#12249=CARTESIAN_POINT ( 'NONE',  ( 1.561832610794586740E-12, -63.51249999999981810, -18.62500000000000000 ) ) ;
#12251=CARTESIAN_POINT ( 'NONE',  ( -7.714727599197334307, -81.20312499999978684, -18.62500000000064659 ) ) ;
#12274=CARTESIAN_POINT ( 'NONE',  ( 13.16986379960055409, -42.63124999999990905, -13.16986379959834430 ) ) ;
#12289=CARTESIAN_POINT ( 'NONE',  ( 3.816460439845750230, 8.305967389184013400E-17, -15.37564352525922473 ) ) ;
#12305=CARTESIAN_POINT ( 'NONE',  ( 11.37499999999960210, -15.60937499999996270, 4.711679271994917428 ) ) ;
#12322=CARTESIAN_POINT ( 'NONE',  ( 18.62362042714189059, -100.0000000000000000, 0.000000000000000000 ) ) ;
#12324=CARTESIAN_POINT ( 'NONE',  ( -8.043339635997654113, -43.70624999999989768, 8.043339635996302306 ) ) ;
#12333=CARTESIAN_POINT ( 'NONE',  ( 13.16986379960055409, -59.28124999999987921, -13.16986379959834430 ) ) ;
#12341=CARTESIAN_POINT ( 'NONE',  ( -7.714727599200466912, -70.79687499999981526, 18.62499999999935341 ) ) ;
#12343=CARTESIAN_POINT ( 'NONE',  ( 13.16986379960055409, -61.43124999999983515, -13.16986379959834430 ) ) ;
#12364=CARTESIAN_POINT ( 'NONE',  ( -13.16986379960055409, -17.65624999999997513, 13.16986379959834252 ) ) ;
#12372=EDGE_CURVE ( 'NONE', #13643, #7272, #9094, .T. ) ;
#12395=CARTESIAN_POINT ( 'NONE',  ( 9.538709233711902776E-13, -20.81249999999995026, -11.37500000000000000 ) ) ;
#12414=CARTESIAN_POINT ( 'NONE',  ( 9.538709233711902776E-13, -70.76249999999983231, -11.37500000000000000 ) ) ;
#12425=CARTESIAN_POINT ( 'NONE',  ( 1.561832610794586740E-12, -61.36249999999986215, -18.62500000000000000 ) ) ;
#12432=CARTESIAN_POINT ( 'NONE',  ( 18.62500000000000000, -92.64999999999974989, 1.560692158462880521E-12 ) ) ;
#12457=CARTESIAN_POINT ( 'NONE',  ( -13.16986379959834252, -80.09374999999982947, -13.16986379960055409 ) ) ;
#12469=CARTESIAN_POINT ( 'NONE',  ( 9.651058002246328371, 3.646912567499685897E-17, -14.62992131181279021 ) ) ;
#12485=CARTESIAN_POINT ( 'NONE',  ( 4.711679271994910323, -69.72187499999984084, -11.37499999999960387 ) ) ;
#12492=CARTESIAN_POINT ( 'NONE',  ( -7.714727599197334307, -5.203124999999987566, -18.62500000000064304 ) ) ;
#12505=CARTESIAN_POINT ( 'NONE',  ( -4.711679271993004292, -88.45312499999978684, -11.37500000000039435 ) ) ;
#12515=CARTESIAN_POINT ( 'NONE',  ( -13.16986379960055409, -67.60624999999984652, 13.16986379959834252 ) ) ;
#12523=CARTESIAN_POINT ( 'NONE',  ( -18.62499999999935341, -49.98437499999987210, -7.714727599200458030 ) ) ;
#12528=CARTESIAN_POINT ( 'NONE',  ( 11.37500000000039435, -67.64062499999984368, -4.711679271993004292 ) ) ;
#12544=CARTESIAN_POINT ( 'NONE',  ( -18.62500000000000000, -65.52499999999986358, -1.562973063126292757E-12 ) ) ;
#12557=CARTESIAN_POINT ( 'NONE',  ( 8.834039747090045580, 3.646912567496566199E-17, -14.96760085455396805 ) ) ;
#12571=CARTESIAN_POINT ( 'NONE',  ( -18.62499999999935341, -83.28437499999976978, -7.714727599200458030 ) ) ;
#12572=CARTESIAN_POINT ( 'NONE',  ( -11.37500000000000000, -24.97499999999994102, -9.545674412382054647E-13 ) ) ;
#12596=CARTESIAN_POINT ( 'NONE',  ( -7.714727599197334307, -79.05312499999985221, -18.62500000000064659 ) ) ;
#12599=EDGE_CURVE ( 'NONE', #13643, #2583, #8830, .T. ) ;
#12605=CARTESIAN_POINT ( 'NONE',  ( 9.538709233711902776E-13, 3.087500000000011458, -11.37500000000000178 ) ) ;
#12611=CARTESIAN_POINT ( 'NONE',  ( 9.538709233711902776E-13, -20.81249999999995026, -11.37500000000000000 ) ) ;
#12628=CARTESIAN_POINT ( 'NONE',  ( -18.62500000000000000, -98.82499999999978968, -1.562973063126292757E-12 ) ) ;
#12633=CARTESIAN_POINT ( 'NONE',  ( 15.00000000000000000, 0.000000000000000000, 1.256933281983527907E-12 ) ) ;
#12653=CARTESIAN_POINT ( 'NONE',  ( 7.714727599200456254, -79.12187499999980389, -18.62499999999935341 ) ) ;
#12654=CARTESIAN_POINT ( 'NONE',  ( -8.043339635996302306, -39.54374999999990337, -8.043339635997654113 ) ) ;
#12660=CARTESIAN_POINT ( 'NONE',  ( 7.714727599200458030, -3.121874999999992628, -18.62499999999935341 ) ) ;
#12678=ORIENTED_EDGE ( 'NONE', *, *, #17355, .T. ) ;
#12683=CARTESIAN_POINT ( 'NONE',  ( -18.62500000000064659, -9.365624999999976552, 7.714727599197335195 ) ) ;
#12691=CARTESIAN_POINT ( 'NONE',  ( -11.37499999999960743, -66.63437499999983515, -4.711679271994912099 ) ) ;
#12699=CARTESIAN_POINT ( 'NONE',  ( 11.37499999999960210, -15.60937499999996270, 4.711679271994918317 ) ) ;
#12717=CARTESIAN_POINT ( 'NONE',  ( 13.16986379959833897, -88.41874999999980389, 13.16986379960055409 ) ) ;
#12733=CARTESIAN_POINT ( 'NONE',  ( 15.00000000000000000, -99.89999999999999147, 0.000000000000000000 ) ) ;
#12742=CARTESIAN_POINT ( 'NONE',  ( -7.714727599197334307, -81.20312499999978684, -18.62500000000064659 ) ) ;
#12743=CARTESIAN_POINT ( 'NONE',  ( 4.711679271994910323, -53.07187499999987068, -11.37499999999960387 ) ) ;
#12747=CARTESIAN_POINT ( 'NONE',  ( -7.714727599197334307, -71.80312499999982379, -18.62500000000064304 ) ) ;
#12749=DIRECTION ( 'NONE',  ( 1.000000000000000000, 0.000000000000000000, 0.000000000000000000 ) ) ;
#12768=CARTESIAN_POINT ( 'NONE',  ( 13.16986379960055054, -35.38124999999991616, -13.16986379959834430 ) ) ;
#12778=CARTESIAN_POINT ( 'NONE',  ( 4.711679271994911211, -29.17187499999991118, -11.37499999999960743 ) ) ;
#12788=CARTESIAN_POINT ( 'NONE',  ( -9.552639591052204498E-13, -36.38749999999993179, 11.37499999999999645 ) ) ;
#12803=CARTESIAN_POINT ( 'NONE',  ( -7.714727599197335195, -38.50312499999991189, -18.62500000000064304 ) ) ;
#12805=CARTESIAN_POINT ( 'NONE',  ( -13.16986379959834252, -39.54374999999990337, -13.16986379960055054 ) ) ;
#12822=CARTESIAN_POINT ( 'NONE',  ( 9.538709233711902776E-13, -11.41249999999998899, -11.37499999999999645 ) ) ;
#12832=CARTESIAN_POINT ( 'NONE',  ( -9.552639591052204498E-13, -21.88749999999992824, 11.37500000000000178 ) ) ;
#12833=CARTESIAN_POINT ( 'NONE',  ( -11.37499999999960387, -40.58437499999990905, -4.711679271994911211 ) ) ;
#12838=CARTESIAN_POINT ( 'NONE',  ( 18.62500000000064304, -34.34062499999991758, -7.714727599197334307 ) ) ;
#12857=CARTESIAN_POINT ( 'NONE',  ( -18.62500000000000000, -24.97499999999994102, -1.562973063126292555E-12 ) ) ;
#12866=CARTESIAN_POINT ( 'NONE',  ( 9.538709233711902776E-13, -46.86249999999987637, -11.37500000000000178 ) ) ;
#12873=CARTESIAN_POINT ( 'NONE',  ( 11.37500000000039613, -24.94062499999995808, -4.711679271993002516 ) ) ;
#12886=CARTESIAN_POINT ( 'NONE',  ( 18.62500000000000000, -49.94999999999988205, 1.560692158462880521E-12 ) ) ;
#12888=CARTESIAN_POINT ( 'NONE',  ( 7.714727599200458030, -19.77187499999995168, -18.62499999999934985 ) ) ;
#12906=CARTESIAN_POINT ( 'NONE',  ( 11.37500000000039613, -24.94062499999995808, -4.711679271993002516 ) ) ;
#12915=CARTESIAN_POINT ( 'NONE',  ( -4.711679271993003404, -14.60312499999994706, -11.37500000000039613 ) ) ;
#12920=CARTESIAN_POINT ( 'NONE',  ( 1.561832610794586538E-12, -54.11249999999986926, -18.62500000000000000 ) ) ;
#12939=CARTESIAN_POINT ( 'NONE',  ( 7.714727599200458030, -19.77187499999995168, -18.62499999999934985 ) ) ;
#12949=CARTESIAN_POINT ( 'NONE',  ( -4.711679271994916540, -37.49687499999989626, 11.37499999999960565 ) ) ;
#12957=CARTESIAN_POINT ( 'NONE',  ( 11.37500000000039613, -41.59062499999991758, -4.711679271993002516 ) ) ;
#12966=CARTESIAN_POINT ( 'NONE',  ( 18.62500000000000000, -99.89999999999976410, 0.000000000000000000 ) ) ;
#12968=CARTESIAN_POINT ( 'NONE',  ( -7.714727599200467800, -78.04687499999982947, 18.62499999999934630 ) ) ;
#12970=CARTESIAN_POINT ( 'NONE',  ( 18.62500000000064304, -67.64062499999984368, -7.714727599197335195 ) ) ;
#12972=CARTESIAN_POINT ( 'NONE',  ( -18.62500000000000000, -41.62499999999990052, -1.562973063126292555E-12 ) ) ;
#12990=CARTESIAN_POINT ( 'NONE',  ( -11.37499999999960210, -47.83437499999990195, -4.711679271994911211 ) ) ;
#13001=CARTESIAN_POINT ( 'NONE',  ( 8.043339635997652337, -44.78124999999987921, -8.043339635996304082 ) ) ;
#13004=CARTESIAN_POINT ( 'NONE',  ( 18.62500000000000000, -83.24999999999980105, 1.560692158462880521E-12 ) ) ;
#13028=CARTESIAN_POINT ( 'NONE',  ( -13.16986379960055231, -10.40624999999997513, 13.16986379959834252 ) ) ;
#13039=CARTESIAN_POINT ( 'NONE',  ( 11.37500000000039613, -60.39062499999985079, -4.711679271993004292 ) ) ;
#13047=CARTESIAN_POINT ( 'NONE',  ( -4.711679271993001628, -29.10312499999994884, -11.37500000000039613 ) ) ;
#13056=CARTESIAN_POINT ( 'NONE',  ( 13.16986379960055054, -85.33124999999978400, -13.16986379959834430 ) ) ;
#13058=CARTESIAN_POINT ( 'NONE',  ( -18.62500000000064659, -42.66562499999989200, 7.714727599197335195 ) ) ;
#13060=CARTESIAN_POINT ( 'NONE',  ( -18.62499999999934985, -7.284374999999982947, -7.714727599200458918 ) ) ;
#13076=CARTESIAN_POINT ( 'NONE',  ( 8.043339635997652337, -25.98124999999995310, -8.043339635996302306 ) ) ;
#13087=CARTESIAN_POINT ( 'NONE',  ( 8.043339635996302306, -57.26874999999984794, 8.043339635997654113 ) ) ;
#13091=CARTESIAN_POINT ( 'NONE',  ( 7.714727599197339636, -63.47812499999984226, 18.62500000000063949 ) ) ;
#13113=CARTESIAN_POINT ( 'NONE',  ( -7.714727599200467800, -94.69687499999979252, 18.62499999999934630 ) ) ;
#13120=CARTESIAN_POINT ( 'NONE',  ( 10.73134851898655917, -99.99999999999995737, 4.282261568526099182 ) ) ;
#13121=PLANE ( 'NONE',  #17276 ) ;
#13122=CARTESIAN_POINT ( 'NONE',  ( 11.37500000000039613, -77.04062499999979252, -4.711679271993004292 ) ) ;
#13133=CARTESIAN_POINT ( 'NONE',  ( 4.711679271993006957, -20.77812499999997087, 11.37500000000039257 ) ) ;
#13141=CARTESIAN_POINT ( 'NONE',  ( -18.62500000000000000, -1.074999999999978639, -1.562973063126292757E-12 ) ) ;
#13143=CARTESIAN_POINT ( 'NONE',  ( -18.62499999999934985, -57.23437499999987921, -7.714727599200458918 ) ) ;
#13146=CARTESIAN_POINT ( 'NONE',  ( 18.62500000000064304, -67.64062499999984368, -7.714727599197335195 ) ) ;
#13164=CARTESIAN_POINT ( 'NONE',  ( 4.711679271994911211, -43.67187499999991473, -11.37499999999960210 ) ) ;
#13174=CARTESIAN_POINT ( 'NONE',  ( -4.711679271994916540, -87.44687499999976410, 11.37499999999960565 ) ) ;
#13201=CARTESIAN_POINT ( 'NONE',  ( 13.16986379959834075, -81.16874999999980389, 13.16986379960055231 ) ) ;
#13210=CARTESIAN_POINT ( 'NONE',  ( -4.711679271994916540, -11.44687499999997371, 11.37499999999960210 ) ) ;
#13218=CARTESIAN_POINT ( 'NONE',  ( 11.37499999999960210, -72.80937499999984652, 4.711679271994916540 ) ) ;
#13226=CARTESIAN_POINT ( 'NONE',  ( 7.714727599200458030, -86.37187499999978968, -18.62499999999934985 ) ) ;
#13228=CARTESIAN_POINT ( 'NONE',  ( 18.62499999999934630, -82.20937499999980957, 7.714727599200467800 ) ) ;
#13251=CARTESIAN_POINT ( 'NONE',  ( -4.711679271994915652, -51.99687499999990337, 11.37499999999960210 ) ) ;
#13261=CARTESIAN_POINT ( 'NONE',  ( -11.37500000000000000, -8.324999999999979750, -9.545674412382054647E-13 ) ) ;
#13262=CARTESIAN_POINT ( 'NONE',  ( 7.714727599200458030, -19.77187499999995168, -18.62499999999934985 ) ) ;
#13287=CARTESIAN_POINT ( 'NONE',  ( -1.564113515457998572E-12, -62.43749999999985079, 18.62500000000000000 ) ) ;
#13294=CARTESIAN_POINT ( 'NONE',  ( 10.39543320068206178, -99.99999999999995737, 14.15274258188488332 ) ) ;
#13296=CARTESIAN_POINT ( 'NONE',  ( -11.37500000000039613, -26.01562499999994671, 4.711679271993002516 ) ) ;
#13303=CARTESIAN_POINT ( 'NONE',  ( -8.043339635996300530, -96.74374999999980673, -8.043339635997652337 ) ) ;
#13310=CARTESIAN_POINT ( 'NONE',  ( 18.62500000000064304, -84.29062499999983515, -7.714727599197335195 ) ) ;
#13312=CARTESIAN_POINT ( 'NONE',  ( 18.62500000000000000, -26.04999999999992255, 1.560692158462880521E-12 ) ) ;
#13315=CARTESIAN_POINT ( 'NONE',  ( -18.62500000000064659, -92.61562499999978115, 7.714727599197335195 ) ) ;
#13332=CARTESIAN_POINT ( 'NONE',  ( 13.16986379960055409, -9.331249999999993605, -13.16986379959834430 ) ) ;
#13340=CARTESIAN_POINT ( 'NONE',  ( -11.37499999999960743, -66.63437499999983515, -4.711679271994912099 ) ) ;
#13341=CARTESIAN_POINT ( 'NONE',  ( 18.62500000000000000, -33.29999999999991900, 1.560692158462880521E-12 ) ) ;
#13376=CARTESIAN_POINT ( 'NONE',  ( 14.43775832588806196, -99.99999999999994316, 10.99793653110744174 ) ) ;
#13378=CARTESIAN_POINT ( 'NONE',  ( -8.043339635996302306, -39.54374999999990337, -8.043339635997654113 ) ) ;
#13387=CARTESIAN_POINT ( 'NONE',  ( 9.538709233711902776E-13, -94.66249999999979536, -11.37499999999999645 ) ) ;
#13392=CARTESIAN_POINT ( 'NONE',  ( -1.564113515457998370E-12, -38.53749999999988063, 18.62500000000000000 ) ) ;
#13394=CARTESIAN_POINT ( 'NONE',  ( -18.62499999999935341, -33.33437499999990195, -7.714727599200458030 ) ) ;
#13397=CARTESIAN_POINT ( 'NONE',  ( -7.714727599200467800, -94.69687499999979252, 18.62499999999934630 ) ) ;
#13415=CARTESIAN_POINT ( 'NONE',  ( -11.37499999999960210, -81.13437499999982094, -4.711679271994911211 ) ) ;
#13424=CARTESIAN_POINT ( 'NONE',  ( -11.37499999999960387, -23.93437499999993889, -4.711679271994910323 ) ) ;
#13425=CARTESIAN_POINT ( 'NONE',  ( -7.714727599200467800, -28.09687499999992966, 18.62499999999934630 ) ) ;
#13446=VECTOR ( 'NONE', #6857, 1000.000000000000000 ) ;
#13450=CARTESIAN_POINT ( 'NONE',  ( 18.62499999999934630, -82.20937499999980957, 7.714727599200467800 ) ) ;
#13462=CARTESIAN_POINT ( 'NONE',  ( 6.732494237459348163, -99.99999999999981526, 15.36475110869683469 ) ) ;
#13464=CARTESIAN_POINT ( 'NONE',  ( 11.37500000000000000, -16.64999999999995950, 9.531744055041752924E-13 ) ) ;
#13473=CARTESIAN_POINT ( 'NONE',  ( -11.37499999999999645, -82.17499999999982663, -9.545674412382054647E-13 ) ) ;
#13480=CARTESIAN_POINT ( 'NONE',  ( -7.714727599200466912, -37.49687499999989626, 18.62499999999935341 ) ) ;
#13482=CARTESIAN_POINT ( 'NONE',  ( -18.62500000000000000, -17.72499999999994102, -1.562973063126292757E-12 ) ) ;
#13502=CARTESIAN_POINT ( 'NONE',  ( -7.714727599197334307, -12.45312499999998757, -18.62500000000064659 ) ) ;
#13509=CARTESIAN_POINT ( 'NONE',  ( -11.37500000000039613, -26.01562499999994671, 4.711679271993002516 ) ) ;
#13510=CARTESIAN_POINT ( 'NONE',  ( 18.62500000000064304, -1.040624999999997469, -7.714727599197335195 ) ) ;
#13516=CARTESIAN_POINT ( 'NONE',  ( 3.922300570379358309, 5.783373742538366110E-16, -15.41399705783805807 ) ) ;
#13546=CARTESIAN_POINT ( 'NONE',  ( 3.593849725469707490, -100.0000000000000711, 14.39518146399953480 ) ) ;
#13548=CARTESIAN_POINT ( 'NONE',  ( -9.552639591052204498E-13, -62.43749999999985079, 11.37500000000000000 ) ) ;
#13559=CARTESIAN_POINT ( 'NONE',  ( 11.37499999999999645, -90.49999999999980105, 9.531744055041752924E-13 ) ) ;
#13565=CARTESIAN_POINT ( 'NONE',  ( 13.16986379960055409, -44.78124999999987921, -13.16986379959834430 ) ) ;
#13567=CARTESIAN_POINT ( 'NONE',  ( 7.714727599197338748, -96.77812499999976126, 18.62500000000063949 ) ) ;
#13590=CARTESIAN_POINT ( 'NONE',  ( 11.37499999999999645, -90.49999999999980105, 9.531744055041752924E-13 ) ) ;
#13598=CARTESIAN_POINT ( 'NONE',  ( 7.714727599200458030, -3.121874999999992628, -18.62499999999934985 ) ) ;
#13603=CARTESIAN_POINT ( 'NONE',  ( 8.417131036019558366, -3.230386817174870386E-14, -15.11476970363428407 ) ) ;
#13633=CARTESIAN_POINT ( 'NONE',  ( 17.69225355208303085, -100.0000000000000000, 5.474315037022701169 ) ) ;
#13636=CARTESIAN_POINT ( 'NONE',  ( 11.37499999999960210, -65.55937499999984652, 4.711679271994918317 ) ) ;
#13643=VERTEX_POINT ( 'NONE', #7661 ) ;
#13644=CARTESIAN_POINT ( 'NONE',  ( -13.16986379960055409, -17.65624999999997513, 13.16986379959834252 ) ) ;
#13649=CARTESIAN_POINT ( 'NONE',  ( -13.16986379960055409, -69.75624999999980957, 13.16986379959834252 ) ) ;
#13652=CARTESIAN_POINT ( 'NONE',  ( 1.561832610794586740E-12, -80.16249999999979536, -18.62500000000000000 ) ) ;
#13673=CARTESIAN_POINT ( 'NONE',  ( -9.552639591052204498E-13, -102.9874999999997698, 11.37499999999999645 ) ) ;
#13685=CARTESIAN_POINT ( 'NONE',  ( 3.612098337086700806, 8.305967389344668621E-17, -15.28315401015443165 ) ) ;
#13701=CARTESIAN_POINT ( 'NONE',  ( 11.37500000000000000, -16.64999999999995950, 9.531744055041752924E-13 ) ) ;
#13720=CARTESIAN_POINT ( 'NONE',  ( -9.552639591052204498E-13, -45.78749999999988773, 11.37500000000000000 ) ) ;
#13730=CARTESIAN_POINT ( 'NONE',  ( 7.714727599197340524, -20.77812499999997087, 18.62500000000063949 ) ) ;
#13735=CARTESIAN_POINT ( 'NONE',  ( 7.714727599197340524, -56.22812499999984936, 18.62500000000063949 ) ) ;
#13737=CARTESIAN_POINT ( 'NONE',  ( 13.16986379959833897, -90.56874999999976694, 13.16986379960055409 ) ) ;
#13758=CARTESIAN_POINT ( 'NONE',  ( -18.62499999999935341, -64.48437499999987210, -7.714727599200458030 ) ) ;
#13770=CARTESIAN_POINT ( 'NONE',  ( 3.371388833146295116, 7.495012466571698890E-16, -13.77928291208580980 ) ) ;
#13787=CARTESIAN_POINT ( 'NONE',  ( -11.37499999999960387, -73.88437499999982094, -4.711679271994911211 ) ) ;
#13807=CARTESIAN_POINT ( 'NONE',  ( -11.37500000000000000, -74.92499999999982663, -9.545674412382054647E-13 ) ) ;
#13815=CARTESIAN_POINT ( 'NONE',  ( 18.62500000000064659, -74.89062499999985789, -7.714727599197336083 ) ) ;
#13821=CARTESIAN_POINT ( 'NONE',  ( 13.16986379960055409, -78.08124999999978400, -13.16986379959834430 ) ) ;
#13828=CARTESIAN_POINT ( 'NONE',  ( -11.37500000000039613, -59.31562499999985505, 4.711679271993002516 ) ) ;
#13845=CARTESIAN_POINT ( 'NONE',  ( 18.62500000000000000, -90.49999999999980105, 1.560692158462880521E-12 ) ) ;
#13856=CARTESIAN_POINT ( 'NONE',  ( 14.83981042559783425, 2.881527793022525794E-15, -10.59219708354840250 ) ) ;
#13873=CARTESIAN_POINT ( 'NONE',  ( 11.37500000000000000, -66.59999999999983800, 9.531744055041752924E-13 ) ) ;
#13902=CARTESIAN_POINT ( 'NONE',  ( 7.714727599197340524, -54.07812499999989342, 18.62500000000063949 ) ) ;
#13909=CARTESIAN_POINT ( 'NONE',  ( 11.37500000000039613, 6.209375000000004974, -4.711679271993004292 ) ) ;
#13917=CARTESIAN_POINT ( 'NONE',  ( 8.043339635997654113, -35.38124999999991616, -8.043339635996304082 ) ) ;
#13932=CARTESIAN_POINT ( 'NONE',  ( -18.62500000000000000, -48.87499999999990052, -1.562973063126292757E-12 ) ) ;
#13945=DIRECTION ( 'NONE',  ( 1.000000000000000000, 0.000000000000000000, 0.000000000000000000 ) ) ;
#13959=CARTESIAN_POINT ( 'NONE',  ( -11.37500000000000178, -17.72499999999994102, -9.545674412382054647E-13 ) ) ;
#13960=CARTESIAN_POINT ( 'NONE',  ( 4.711679271993006068, -63.47812499999984226, 11.37500000000039257 ) ) ;
#13966=CARTESIAN_POINT ( 'NONE',  ( -18.62499999999935341, -7.284374999999982947, -7.714727599200458918 ) ) ;
#13969=ADVANCED_FACE ( 'NONE', ( #2666 ), #13121, .F. ) ;
#13987=CARTESIAN_POINT ( 'NONE',  ( -7.714727599200466912, -51.99687499999990337, 18.62499999999935341 ) ) ;
#13996=CARTESIAN_POINT ( 'NONE',  ( -13.16986379960055409, -86.40624999999977263, 13.16986379959834252 ) ) ;
#14004=CARTESIAN_POINT ( 'NONE',  ( -8.043339635997654113, -27.05624999999993463, 8.043339635996302306 ) ) ;
#14025=CARTESIAN_POINT ( 'NONE',  ( -7.714727599197334307, -62.40312499999986073, -18.62500000000064659 ) ) ;
#14034=UNCERTAINTY_MEASURE_WITH_UNIT (LENGTH_MEASURE( 1.000000000000000082E-05 ), #8623, 'distance_accuracy_value', 'NONE');
#14053=CARTESIAN_POINT ( 'NONE',  ( 13.16986379959833897, -90.56874999999976694, 13.16986379960055409 ) ) ;
#14054=CARTESIAN_POINT ( 'NONE',  ( 4.711679271994910323, -36.42187499999990763, -11.37499999999960387 ) ) ;
#14060=CARTESIAN_POINT ( 'NONE',  ( 7.714727599200458030, -53.07187499999987068, -18.62499999999935341 ) ) ;
#14079=CARTESIAN_POINT ( 'NONE',  ( 18.62500000000064304, -34.34062499999991047, -7.714727599197335195 ) ) ;
#14087=CARTESIAN_POINT ( 'NONE',  ( 8.043339635996302306, -7.318749999999964118, 8.043339635997654113 ) ) ;
#14093=ORIENTED_EDGE ( 'NONE', *, *, #4067, .F. ) ;
#14096=CARTESIAN_POINT ( 'NONE',  ( 8.043339635996300530, -97.81874999999976694, 8.043339635997654113 ) ) ;
#14111=CARTESIAN_POINT ( 'NONE',  ( 18.62499999999934630, -32.25937499999992042, 7.714727599200467800 ) ) ;
#14113=CARTESIAN_POINT ( 'NONE',  ( -13.16986379959834252, -96.74374999999980673, -13.16986379960055409 ) ) ;
#14122=CARTESIAN_POINT ( 'NONE',  ( 11.37500000000007816, 4.439344646909156023E-16, -0.9008532055000779692 ) ) ;
#14124=( NAMED_UNIT ( * ) PLANE_ANGLE_UNIT ( ) SI_UNIT ( $, .RADIAN. ) );
#14129=CARTESIAN_POINT ( 'NONE',  ( 11.37500000000000000, -66.59999999999983800, 9.531744055041752924E-13 ) ) ;
#14139=CARTESIAN_POINT ( 'NONE',  ( -18.62500000000064659, -85.36562499999978115, 7.714727599197333419 ) ) ;
#14140=CARTESIAN_POINT ( 'NONE',  ( -9.552639591052204498E-13, -45.78749999999988773, 11.37500000000000000 ) ) ;
#14144=CARTESIAN_POINT ( 'NONE',  ( -18.62500000000064659, -75.96562499999981810, 7.714727599197333419 ) ) ;
#14165=CARTESIAN_POINT ( 'NONE',  ( -7.714727599197335195, -21.85312499999995239, -18.62500000000064304 ) ) ;
#14176=CARTESIAN_POINT ( 'NONE',  ( -11.37500000000000178, -17.72499999999994102, -9.545674412382054647E-13 ) ) ;
#14183=CARTESIAN_POINT ( 'NONE',  ( 11.37499999999999645, -7.250000000000000000, 9.531744055041752924E-13 ) ) ;
#14198=CARTESIAN_POINT ( 'NONE',  ( 7.714727599200458030, -19.77187499999995168, -18.62499999999934985 ) ) ;
#14200=CARTESIAN_POINT ( 'NONE',  ( 18.62499999999934630, -48.90937499999989058, 7.714727599200467800 ) ) ;
#14214=CARTESIAN_POINT ( 'NONE',  ( -11.37500000000039613, -33.26562499999994316, 4.711679271993000739 ) ) ;
#14224=CARTESIAN_POINT ( 'NONE',  ( 4.711679271993006957, -6.278124999999967315, 11.37500000000039613 ) ) ;
#14229=CARTESIAN_POINT ( 'NONE',  ( -1.564113515457998572E-12, -79.08749999999980673, 18.62500000000000000 ) ) ;
#14249=CARTESIAN_POINT ( 'NONE',  ( 18.62500000000000000, -33.29999999999991900, 1.560692158462880521E-12 ) ) ;
#14258=CARTESIAN_POINT ( 'NONE',  ( 11.37500000000000178, -9.399999999999959499, 9.531744055041752924E-13 ) ) ;
#14267=CARTESIAN_POINT ( 'NONE',  ( 8.043339635996298753, -38.46874999999992895, 8.043339635997652337 ) ) ;
#14278=CARTESIAN_POINT ( 'NONE',  ( 1.561832610794586538E-12, -70.76249999999983231, -18.62500000000000000 ) ) ;
#14280=CARTESIAN_POINT ( 'NONE',  ( -13.16986379960055231, -60.35624999999985363, 13.16986379959834252 ) ) ;
#14282=CARTESIAN_POINT ( 'NONE',  ( -13.16986379959834252, -22.89374999999994387, -13.16986379960055054 ) ) ;
#14300=CARTESIAN_POINT ( 'NONE',  ( 9.538709233711902776E-13, -44.71249999999991331, -11.37499999999999645 ) ) ;
#14309=CARTESIAN_POINT ( 'NONE',  ( 1.561832610794586740E-12, -80.16249999999979536, -18.62500000000000000 ) ) ;
#14314=CARTESIAN_POINT ( 'NONE',  ( -18.62500000000064659, -26.01562499999994316, 7.714727599197333419 ) ) ;
#14334=CARTESIAN_POINT ( 'NONE',  ( -7.714727599197335195, -5.203124999999987566, -18.62500000000064304 ) ) ;
#14342=CARTESIAN_POINT ( 'NONE',  ( 10.12542398630638552, -99.99999999999998579, 5.924228240590371897 ) ) ;
#14344=CARTESIAN_POINT ( 'NONE',  ( 11.37499999999960565, -41.65937499999989058, 4.711679271994918317 ) ) ;
#14351=CARTESIAN_POINT ( 'NONE',  ( -8.043339635996302306, -89.49374999999979252, -8.043339635997654113 ) ) ;
#14360=CARTESIAN_POINT ( 'NONE',  ( -18.62500000000000000, -91.57499999999977547, -1.562973063126292555E-12 ) ) ;
#14363=CARTESIAN_POINT ( 'NONE',  ( 1.561832610794586538E-12, -20.81249999999995026, -18.62500000000000000 ) ) ;
#14365=CARTESIAN_POINT ( 'NONE',  ( 7.714727599200458030, -36.42187499999990763, -18.62499999999934985 ) ) ;
#14384=CARTESIAN_POINT ( 'NONE',  ( 8.043339635996298753, -71.76874999999985505, 8.043339635997652337 ) ) ;
#14393=CARTESIAN_POINT ( 'NONE',  ( 9.538709233711902776E-13, -4.162499999999988987, -11.37500000000000000 ) ) ;
#14396=CARTESIAN_POINT ( 'NONE',  ( 7.714727599197339636, -80.12812499999981242, 18.62500000000063949 ) ) ;
#14421=CARTESIAN_POINT ( 'NONE',  ( 13.16986379960055054, -2.081249999999994937, -13.16986379959834430 ) ) ;
#14431=CARTESIAN_POINT ( 'NONE',  ( -4.711679271993003404, -64.55312499999983800, -11.37500000000039613 ) ) ;
#14441=CARTESIAN_POINT ( 'NONE',  ( 9.538709233711902776E-13, -11.41249999999998899, -11.37499999999999645 ) ) ;
#14450=CARTESIAN_POINT ( 'NONE',  ( 7.714727599197338748, -46.82812499999989342, 18.62500000000063949 ) ) ;
#14452=CARTESIAN_POINT ( 'NONE',  ( -18.62500000000064659, -59.31562499999985505, 7.714727599197335195 ) ) ;
#14455=CARTESIAN_POINT ( 'NONE',  ( 18.62500000000000000, -49.94999999999988205, 1.560692158462880521E-12 ) ) ;
#14472=CARTESIAN_POINT ( 'NONE',  ( 11.37499999999999645, -57.19999999999988916, 9.531744055041752924E-13 ) ) ;
#14481=CARTESIAN_POINT ( 'NONE',  ( -11.37500000000000178, -84.32499999999977547, -9.545674412382054647E-13 ) ) ;
#14485=CARTESIAN_POINT ( 'NONE',  ( 13.16986379959834075, -97.81874999999976694, 13.16986379960055231 ) ) ;
#14506=CARTESIAN_POINT ( 'NONE',  ( 7.714727599200458030, -86.37187499999978968, -18.62499999999934985 ) ) ;
#14514=CARTESIAN_POINT ( 'NONE',  ( 4.878238517571312549, -99.99999999999998579, 12.54298690192642596 ) ) ;
#14516=CARTESIAN_POINT ( 'NONE',  ( 8.043339635996302306, -90.56874999999976694, 8.043339635997654113 ) ) ;
#14525=CARTESIAN_POINT ( 'NONE',  ( -11.37499999999999645, -65.52499999999986358, -9.545674412382054647E-13 ) ) ;
#14533=CARTESIAN_POINT ( 'NONE',  ( 18.62499999999934630, -65.55937499999984652, 7.714727599200467800 ) ) ;
#14535=CARTESIAN_POINT ( 'NONE',  ( 18.62500000000064659, 6.209375000000004974, -7.714727599197336083 ) ) ;
#14538=CARTESIAN_POINT ( 'NONE',  ( -7.714727599200467800, -44.74687499999989626, 18.62499999999934630 ) ) ;
#14559=CARTESIAN_POINT ( 'NONE',  ( 4.711679271993006957, -54.07812499999989342, 11.37500000000039257 ) ) ;
#14570=CARTESIAN_POINT ( 'NONE',  ( 8.043339635997654113, -2.081249999999994493, -8.043339635996304082 ) ) ;
#14599=CARTESIAN_POINT ( 'NONE',  ( -18.62499999999934985, -40.58437499999990905, -7.714727599200458918 ) ) ;
#14608=CARTESIAN_POINT ( 'NONE',  ( -11.37500000000039790, -68.71562499999981810, 4.711679271993001628 ) ) ;
#14609=CARTESIAN_POINT ( 'NONE',  ( 15.00000000000000000, -99.89999999999999147, 0.000000000000000000 ) ) ;
#14616=CARTESIAN_POINT ( 'NONE',  ( -4.711679271994915652, -51.99687499999990337, 11.37499999999960210 ) ) ;
#14622=CARTESIAN_POINT ( 'NONE',  ( -13.16986379959834252, -72.84374999999981526, -13.16986379960055054 ) ) ;
#14624=CARTESIAN_POINT ( 'NONE',  ( -7.714727599200466912, -20.84687499999993321, 18.62499999999935341 ) ) ;
#14628=CARTESIAN_POINT ( 'NONE',  ( 1.561832610794586538E-12, -87.41249999999979536, -18.62500000000000000 ) ) ;
#14646=CARTESIAN_POINT ( 'NONE',  ( -8.043339635997652337, -100.9062499999997868, 8.043339635996300530 ) ) ;
#14655=CARTESIAN_POINT ( 'NONE',  ( 9.538709233711902776E-13, -63.51249999999981810, -11.37500000000000178 ) ) ;
#14656=CARTESIAN_POINT ( 'NONE',  ( -7.714727599200467800, -11.44687499999997371, 18.62499999999934630 ) ) ;
#14681=CARTESIAN_POINT ( 'NONE',  ( -7.714727599197335195, -55.15312499999986784, -18.62500000000064304 ) ) ;
#14692=CARTESIAN_POINT ( 'NONE',  ( -4.711679271994916540, -87.44687499999976410, 11.37499999999960565 ) ) ;
#14699=ORIENTED_EDGE ( 'NONE', *, *, #12599, .T. ) ;
#14700=CARTESIAN_POINT ( 'NONE',  ( 11.37499999999960210, -89.45937499999983800, 4.711679271994916540 ) ) ;
#14706=CARTESIAN_POINT ( 'NONE',  ( 18.62499999999935341, -58.30937499999983231, 7.714727599200469577 ) ) ;
#14708=CARTESIAN_POINT ( 'NONE',  ( -13.16986379959834252, -89.49374999999979252, -13.16986379960055054 ) ) ;
#14709=AXIS2_PLACEMENT_3D ( 'NONE', #9368, #1041, #17125 ) ;
#14712=CARTESIAN_POINT ( 'NONE',  ( 18.62500000000000000, -83.24999999999980105, 1.560692158462880521E-12 ) ) ;
#14729=CARTESIAN_POINT ( 'NONE',  ( 1.561832610794586740E-12, -11.41249999999999254, -18.62500000000000000 ) ) ;
#14739=CARTESIAN_POINT ( 'NONE',  ( 11.37500000000000000, -33.29999999999991900, 9.531744055041752924E-13 ) ) ;
#14740=CARTESIAN_POINT ( 'NONE',  ( 18.62500000000064304, -17.69062499999995453, -7.714727599197335195 ) ) ;
#14764=CARTESIAN_POINT ( 'NONE',  ( -7.714727599200467800, -61.39687499999984510, 18.62499999999934630 ) ) ;
#14777=CARTESIAN_POINT ( 'NONE',  ( -4.711679271994916540, -70.79687499999981526, 11.37499999999960565 ) ) ;
#14786=CARTESIAN_POINT ( 'NONE',  ( -8.043339635996300530, -63.44374999999985931, -8.043339635997652337 ) ) ;
#14791=CARTESIAN_POINT ( 'NONE',  ( 18.62500000000064659, -27.09062499999992113, -7.714727599197336083 ) ) ;
#14793=CARTESIAN_POINT ( 'NONE',  ( 18.62500000000000000, 7.250000000000001776, 1.560692158462880521E-12 ) ) ;
#14813=CARTESIAN_POINT ( 'NONE',  ( -13.16986379959834252, -30.14374999999995097, -13.16986379960055409 ) ) ;
#14823=CARTESIAN_POINT ( 'NONE',  ( -4.711679271993004292, -55.15312499999986784, -11.37500000000039435 ) ) ;
#14824=CARTESIAN_POINT ( 'NONE',  ( -18.62500000000000000, -41.62499999999990052, -1.562973063126292555E-12 ) ) ;
#14849=CARTESIAN_POINT ( 'NONE',  ( -13.16986379959834252, -56.19374999999985931, -13.16986379960055054 ) ) ;
#14860=CARTESIAN_POINT ( 'NONE',  ( -8.043339635996302306, -72.84374999999981526, -8.043339635997654113 ) ) ;
#14869=CARTESIAN_POINT ( 'NONE',  ( 4.711679271993006957, -54.07812499999989342, 11.37500000000039257 ) ) ;
#14876=CARTESIAN_POINT ( 'NONE',  ( -13.16986379960055409, -36.45624999999989768, 13.16986379959834252 ) ) ;
#14878=CARTESIAN_POINT ( 'NONE',  ( 18.62500000000064659, -27.09062499999992113, -7.714727599197336083 ) ) ;
#14881=CARTESIAN_POINT ( 'NONE',  ( 18.62500000000064304, -84.29062499999983515, -7.714727599197335195 ) ) ;
#14904=CARTESIAN_POINT ( 'NONE',  ( 13.16986379959833897, -38.46874999999992895, 13.16986379960055409 ) ) ;
#14913=CARTESIAN_POINT ( 'NONE',  ( 13.16986379960055054, -2.081249999999994937, -13.16986379959834430 ) ) ;
#14919=CARTESIAN_POINT ( 'NONE',  ( 5.796175271902052728, -7.251940901129036557E-16, -15.63158725347429545 ) ) ;
#14954=CARTESIAN_POINT ( 'NONE',  ( 8.043339635997654113, -52.03124999999987921, -8.043339635996304082 ) ) ;
#14956=CARTESIAN_POINT ( 'NONE',  ( 4.711679271993006068, -46.82812499999989342, 11.37500000000039257 ) ) ;
#14963=CARTESIAN_POINT ( 'NONE',  ( -18.62500000000000000, -32.22499999999993747, -1.562973063126292757E-12 ) ) ;
#14971=CARTESIAN_POINT ( 'NONE',  ( -13.16986379959834252, -48.94374999999985931, -13.16986379960055409 ) ) ;
#14973=CARTESIAN_POINT ( 'NONE',  ( -13.16986379959834252, -65.59374999999981526, -13.16986379960055409 ) ) ;
#14994=CARTESIAN_POINT ( 'NONE',  ( -11.37499999999960210, -97.78437499999979821, -4.711679271994911211 ) ) ;
#15007=CARTESIAN_POINT ( 'NONE',  ( 4.958022057362319046, -6.117673133592627308E-13, -12.22358761560111695 ) ) ;
#15039=CARTESIAN_POINT ( 'NONE',  ( 11.37500000000039613, -8.290625000000000355, -4.711679271993002516 ) ) ;
#15048=CARTESIAN_POINT ( 'NONE',  ( -1.564113515457998370E-12, -53.03749999999988773, 18.62500000000000000 ) ) ;
#15052=CARTESIAN_POINT ( 'NONE',  ( 18.62500000000064659, -10.44062499999995453, -7.714727599197336083 ) ) ;
#15054=CARTESIAN_POINT ( 'NONE',  ( -18.62499999999935341, -66.63437499999983515, -7.714727599200458030 ) ) ;
#15076=CARTESIAN_POINT ( 'NONE',  ( -13.16986379960055409, -50.95624999999989768, 13.16986379959834252 ) ) ;
#15088=CARTESIAN_POINT ( 'NONE',  ( 15.12110384299646881, 2.066541229842317853E-14, -10.24447576295584383 ) ) ;
#15104=CARTESIAN_POINT ( 'NONE',  ( -8.043339635996302306, -56.19374999999985931, -8.043339635997654113 ) ) ;
#15124=CARTESIAN_POINT ( 'NONE',  ( 8.043339635997654113, -85.33124999999978400, -8.043339635996304082 ) ) ;
#15135=CARTESIAN_POINT ( 'NONE',  ( 18.62500000000000000, -73.84999999999983800, 1.560692158462880521E-12 ) ) ;
#15143=CARTESIAN_POINT ( 'NONE',  ( -7.714727599200466912, -54.14687499999985931, 18.62499999999935341 ) ) ;
#15149=CARTESIAN_POINT ( 'NONE',  ( 8.043339635996300530, -64.51874999999984084, 8.043339635997654113 ) ) ;
#15168=CARTESIAN_POINT ( 'NONE',  ( 18.62499999999935341, -72.80937499999984652, 7.714727599200469577 ) ) ;
#15180=CARTESIAN_POINT ( 'NONE',  ( 10.51254708004915983, -1.361280322109189478E-15, -4.824314191992851164 ) ) ;
#15197=CARTESIAN_POINT ( 'NONE',  ( 11.37500000000039435, -50.99062499999988063, -4.711679271993003404 ) ) ;
#15227=CARTESIAN_POINT ( 'NONE',  ( -7.714727599200466912, -18.69687499999997726, 18.62499999999935341 ) ) ;
#15232=CIRCLE ( 'NONE', #7087, 3.624999999999999556 ) ;
#15235=CARTESIAN_POINT ( 'NONE',  ( -13.16986379959834252, -82.24374999999977831, -13.16986379960055409 ) ) ;
#15241=CARTESIAN_POINT ( 'NONE',  ( 9.538709233711902776E-13, -54.11249999999986926, -11.37500000000000000 ) ) ;
#15256=CARTESIAN_POINT ( 'NONE',  ( -18.62500000000064659, -99.86562499999978115, 7.714727599197333419 ) ) ;
#15270=CARTESIAN_POINT ( 'NONE',  ( 4.246271870433876217, 5.783373742538367096E-16, -15.51202266832556198 ) ) ;
#15284=CARTESIAN_POINT ( 'NONE',  ( 4.711679271994911211, 4.128125000000008704, -11.37499999999960743 ) ) ;
#15285=CARTESIAN_POINT ( 'NONE',  ( 11.37499999999960210, -82.20937499999980957, 4.711679271994917428 ) ) ;
#15291=CARTESIAN_POINT ( 'NONE',  ( 18.62499999999934985, -15.60937499999996270, 7.714727599200467800 ) ) ;
#15312=CARTESIAN_POINT ( 'NONE',  ( 18.62500000000064659, -24.94062499999996518, -7.714727599197336083 ) ) ;
#15318=CARTESIAN_POINT ( 'NONE',  ( -18.62500000000064659, -68.71562499999981810, 7.714727599197333419 ) ) ;
#15326=CARTESIAN_POINT ( 'NONE',  ( -4.711679271994916540, -28.09687499999992966, 11.37499999999960210 ) ) ;
#15344=CARTESIAN_POINT ( 'NONE',  ( -18.62500000000064659, -83.21562499999981810, 7.714727599197333419 ) ) ;
#15370=CARTESIAN_POINT ( 'NONE',  ( 9.538709233711902776E-13, -30.21249999999990976, -11.37500000000000178 ) ) ;
#15371=CARTESIAN_POINT ( 'NONE',  ( 8.043339635997654113, -35.38124999999991616, -8.043339635996304082 ) ) ;
#15376=CARTESIAN_POINT ( 'NONE',  ( -18.62499999999935341, -40.58437499999990905, -7.714727599200458918 ) ) ;
#15396=STYLED_ITEM('',(#17519),#3202);
#15399=CARTESIAN_POINT ( 'NONE',  ( 18.62499999999934630, -32.25937499999992042, 7.714727599200467800 ) ) ;
#15409=CARTESIAN_POINT ( 'NONE',  ( 8.043339635996302306, -40.61874999999988489, 8.043339635997654113 ) ) ;
#15416=CARTESIAN_POINT ( 'NONE',  ( -8.043339635996300530, -13.49374999999998614, -8.043339635997652337 ) ) ;
#15431=CARTESIAN_POINT ( 'NONE',  ( 1.561832610794586538E-12, -37.46249999999991331, -18.62500000000000000 ) ) ;
#15433=CARTESIAN_POINT ( 'NONE',  ( 7.714727599200458030, -3.121874999999992628, -18.62499999999934985 ) ) ;
#15449=CARTESIAN_POINT ( 'NONE',  ( 11.37500000000039435, -67.64062499999984368, -4.711679271993004292 ) ) ;
#15458=CARTESIAN_POINT ( 'NONE',  ( 13.16986379959833897, -73.91874999999977547, 13.16986379960055409 ) ) ;
#15459=CARTESIAN_POINT ( 'NONE',  ( 9.538709233711902776E-13, -70.76249999999983231, -11.37500000000000000 ) ) ;
#15464=CARTESIAN_POINT ( 'NONE',  ( 13.16986379960055054, -35.38124999999991616, -13.16986379959834430 ) ) ;
#15484=CARTESIAN_POINT ( 'NONE',  ( 7.714727599200458030, -3.121874999999992628, -18.62499999999934985 ) ) ;
#15493=CARTESIAN_POINT ( 'NONE',  ( 11.37500000000039613, -43.74062499999988773, -4.711679271993004292 ) ) ;
#15500=CARTESIAN_POINT ( 'NONE',  ( 11.37499999999960210, -82.20937499999980957, 4.711679271994918317 ) ) ;
#15514=CARTESIAN_POINT ( 'NONE',  ( -18.62500000000000000, -24.97499999999994102, -1.562973063126292555E-12 ) ) ;
#15516=CARTESIAN_POINT ( 'NONE',  ( -18.62499999999934985, -23.93437499999993889, -7.714727599200458918 ) ) ;
#15534=CARTESIAN_POINT ( 'NONE',  ( 4.711679271994911211, -27.02187499999995524, -11.37499999999960210 ) ) ;
#15544=CARTESIAN_POINT ( 'NONE',  ( 11.37500000000000178, 7.250000000000001776, 9.531744055041752924E-13 ) ) ;
#15549=CARTESIAN_POINT ( 'NONE',  ( 18.62500000000000000, -33.29999999999991900, 1.560692158462880521E-12 ) ) ;
#15569=CARTESIAN_POINT ( 'NONE',  ( 18.62499999999935341, -89.45937499999983800, 7.714727599200469577 ) ) ;
#15580=CARTESIAN_POINT ( 'NONE',  ( -8.043339635996304082, -48.94374999999985931, -8.043339635997652337 ) ) ;
#15589=CARTESIAN_POINT ( 'NONE',  ( -4.711679271993001628, -12.45312499999998757, -11.37500000000039613 ) ) ;
#15598=CARTESIAN_POINT ( 'NONE',  ( 18.62499999999934630, -48.90937499999989058, 7.714727599200467800 ) ) ;
#15600=CARTESIAN_POINT ( 'NONE',  ( -13.16986379959834252, -22.89374999999994387, -13.16986379960055054 ) ) ;
#15603=CARTESIAN_POINT ( 'NONE',  ( -18.62500000000064659, -9.365624999999976552, 7.714727599197335195 ) ) ;
#15619=CARTESIAN_POINT ( 'NONE',  ( 4.711679271993006957, -70.72812499999983515, 11.37500000000039257 ) ) ;
#15628=CARTESIAN_POINT ( 'NONE',  ( -8.043339635996304082, 1.006250000000015854, -8.043339635997652337 ) ) ;
#15629=CARTESIAN_POINT ( 'NONE',  ( 4.711679271993006068, -96.77812499999977547, 11.37500000000039257 ) ) ;
#15633=CARTESIAN_POINT ( 'NONE',  ( -18.62499999999935341, -73.88437499999982094, -7.714727599200458918 ) ) ;
#15654=CARTESIAN_POINT ( 'NONE',  ( 13.16986379959833897, -88.41874999999980389, 13.16986379960055409 ) ) ;
#15665=CARTESIAN_POINT ( 'NONE',  ( -9.552639591052204498E-13, -55.18749999999985079, 11.37500000000000178 ) ) ;
#15673=CARTESIAN_POINT ( 'NONE',  ( 4.711679271994911211, -43.67187499999991473, -11.37499999999960210 ) ) ;
#15679=MECHANICAL_DESIGN_GEOMETRIC_PRESENTATION_REPRESENTATION('',(#15396),#5272);
#15684=CARTESIAN_POINT ( 'NONE',  ( -7.714727599197335195, -88.45312499999978684, -18.62500000000064304 ) ) ;
#15686=CARTESIAN_POINT ( 'NONE',  ( 7.714727599197338748, -13.52812499999996732, 18.62500000000063949 ) ) ;
#15688=CARTESIAN_POINT ( 'NONE',  ( -18.62500000000064659, -59.31562499999985505, 7.714727599197335195 ) ) ;
#15710=CARTESIAN_POINT ( 'NONE',  ( -11.37499999999960210, -14.53437499999998295, -4.711679271994911211 ) ) ;
#15719=CARTESIAN_POINT ( 'NONE',  ( -11.37499999999960743, -83.28437499999976978, -4.711679271994912099 ) ) ;
#15723=CARTESIAN_POINT ( 'NONE',  ( 1.561832610794586538E-12, -37.46249999999991331, -18.62500000000000000 ) ) ;
#15743=ORIENTED_EDGE ( 'NONE', *, *, #10854, .T. ) ;
#15745=CARTESIAN_POINT ( 'NONE',  ( -7.714727599197334307, -95.70312499999980105, -18.62500000000064659 ) ) ;
#15754=CARTESIAN_POINT ( 'NONE',  ( 9.073745536650823951, -100.0000000000000995, 7.819101196815612553 ) ) ;
#15756=CARTESIAN_POINT ( 'NONE',  ( -9.552639591052204498E-13, -21.88749999999992824, 11.37500000000000178 ) ) ;
#15764=CARTESIAN_POINT ( 'NONE',  ( -8.043339635997654113, -77.00624999999982379, 8.043339635996302306 ) ) ;
#15773=CARTESIAN_POINT ( 'NONE',  ( 18.62500000000000000, -49.94999999999988205, 1.560692158462880521E-12 ) ) ;
#15775=CARTESIAN_POINT ( 'NONE',  ( -13.16986379959834252, -72.84374999999981526, -13.16986379960055054 ) ) ;
#15778=CARTESIAN_POINT ( 'NONE',  ( -18.62499999999934985, -40.58437499999990905, -7.714727599200458918 ) ) ;
#15790=PLANE ( 'NONE',  #14709 ) ;
#15800=CARTESIAN_POINT ( 'NONE',  ( -4.711679271993001628, -79.05312499999985221, -11.37500000000039613 ) ) ;
#15810=CARTESIAN_POINT ( 'NONE',  ( 4.711679271994911211, -79.12187499999980389, -11.37499999999960743 ) ) ;
#15845=CARTESIAN_POINT ( 'NONE',  ( 5.665088118870674982, -100.0000000000000000, 11.78543286343676044 ) ) ;
#15847=CARTESIAN_POINT ( 'NONE',  ( -9.552639591052204498E-13, -71.83749999999979252, 11.37500000000000178 ) ) ;
#15858=CARTESIAN_POINT ( 'NONE',  ( 11.37499999999960210, -56.15937499999989058, 4.711679271994916540 ) ) ;
#15865=CARTESIAN_POINT ( 'NONE',  ( -7.714727599200466912, -4.196874999999971934, 18.62499999999935341 ) ) ;
#15867=CARTESIAN_POINT ( 'NONE',  ( 7.714727599197338748, -80.12812499999981242, 18.62500000000063949 ) ) ;
#15870=CARTESIAN_POINT ( 'NONE',  ( 13.16986379959834075, -64.51874999999984084, 13.16986379960055231 ) ) ;
#15887=CARTESIAN_POINT ( 'NONE',  ( -9.552639591052204498E-13, -19.73749999999997229, 11.37499999999999645 ) ) ;
#15898=CARTESIAN_POINT ( 'NONE',  ( 11.37500000000000178, -92.64999999999974989, 9.531744055041752924E-13 ) ) ;
#15923=CARTESIAN_POINT ( 'NONE',  ( 13.16986379960055054, -68.68124999999983515, -13.16986379959834430 ) ) ;
#15931=CARTESIAN_POINT ( 'NONE',  ( 3.989780539755591882, -100.0000000000000568, 13.50333144898421089 ) ) ;
#15933=CARTESIAN_POINT ( 'NONE',  ( -8.043339635996302306, -22.89374999999994387, -8.043339635997654113 ) ) ;
#15941=CARTESIAN_POINT ( 'NONE',  ( 11.37500000000039613, -74.89062499999985789, -4.711679271993002516 ) ) ;
#15950=CARTESIAN_POINT ( 'NONE',  ( 13.16986379960055409, 5.168750000000006395, -13.16986379959834430 ) ) ;
#15952=CARTESIAN_POINT ( 'NONE',  ( 1.561832610794586538E-12, -87.41249999999979536, -18.62500000000000000 ) ) ;
#15954=CARTESIAN_POINT ( 'NONE',  ( -13.16986379959834252, -72.84374999999981526, -13.16986379960055054 ) ) ;
#15975=CARTESIAN_POINT ( 'NONE',  ( 8.043339635996298753, -88.41874999999980389, 8.043339635997652337 ) ) ;
#15984=CARTESIAN_POINT ( 'NONE',  ( 4.711679271993006957, -39.57812499999989342, 11.37500000000039613 ) ) ;
#15988=CARTESIAN_POINT ( 'NONE',  ( -13.16986379960055231, -93.65624999999977263, 13.16986379959834252 ) ) ;
#16008=CARTESIAN_POINT ( 'NONE',  ( 7.714727599197338748, -80.12812499999981242, 18.62500000000063949 ) ) ;
#16017=CARTESIAN_POINT ( 'NONE',  ( 7.585183428008853923, -99.99999999999978684, 15.21066662881120202 ) ) ;
#16019=CARTESIAN_POINT ( 'NONE',  ( -4.711679271993004292, -38.50312499999991189, -11.37500000000039435 ) ) ;
#16029=CARTESIAN_POINT ( 'NONE',  ( -11.37499999999999645, -98.82499999999978968, -9.545674412382054647E-13 ) ) ;
#16034=CARTESIAN_POINT ( 'NONE',  ( -1.564113515457998370E-12, -5.237499999999969624, 18.62500000000000000 ) ) ;
#16036=CARTESIAN_POINT ( 'NONE',  ( -7.714727599200467800, -78.04687499999982947, 18.62499999999934630 ) ) ;
#16040=CARTESIAN_POINT ( 'NONE',  ( -13.16986379959834252, -89.49374999999979252, -13.16986379960055054 ) ) ;
#16060=CARTESIAN_POINT ( 'NONE',  ( 18.62499999999935341, -22.85937499999996803, 7.714727599200469577 ) ) ;
#16070=CARTESIAN_POINT ( 'NONE',  ( 8.043339635997652337, -61.43124999999983515, -8.043339635996304082 ) ) ;
#16071=CARTESIAN_POINT ( 'NONE',  ( -18.62500000000000000, -24.97499999999994102, -1.562973063126292555E-12 ) ) ;
#16092=CARTESIAN_POINT ( 'NONE',  ( 1.561832610794586538E-12, -87.41249999999979536, -18.62500000000000000 ) ) ;
#16102=CARTESIAN_POINT ( 'NONE',  ( 18.28286893203052799, -100.0000000000000142, 3.421288217922580976 ) ) ;
#16104=CARTESIAN_POINT ( 'NONE',  ( -11.37499999999960387, -23.93437499999993889, -4.711679271994910323 ) ) ;
#16112=CARTESIAN_POINT ( 'NONE',  ( -18.62499999999935341, -14.53437499999998650, -7.714727599200458030 ) ) ;
#16118=CARTESIAN_POINT ( 'NONE',  ( 13.16986379959833897, -23.96874999999992539, 13.16986379960055409 ) ) ;
#16120=CARTESIAN_POINT ( 'NONE',  ( -1.564113515457998572E-12, -95.73749999999976978, 18.62500000000000000 ) ) ;
#16123=CARTESIAN_POINT ( 'NONE',  ( -18.62500000000000000, -91.57499999999977547, -1.562973063126292555E-12 ) ) ;
#16142=CARTESIAN_POINT ( 'NONE',  ( 18.62500000000000000, -7.250000000000001776, 1.560692158462880521E-12 ) ) ;
#16152=CARTESIAN_POINT ( 'NONE',  ( 9.538709233711902776E-13, -37.46249999999991331, -11.37500000000000000 ) ) ;
#16153=CARTESIAN_POINT ( 'NONE',  ( 1.561832610794586538E-12, -37.46249999999991331, -18.62500000000000000 ) ) ;
#16173=CARTESIAN_POINT ( 'NONE',  ( 8.043339635997654113, -2.081249999999994493, -8.043339635996304082 ) ) ;
#16176=CARTESIAN_POINT ( 'NONE',  ( -18.62500000000064659, -92.61562499999978115, 7.714727599197335195 ) ) ;
#16188=CARTESIAN_POINT ( 'NONE',  ( 8.043339635997654113, -2.081249999999994493, -8.043339635996304082 ) ) ;
#16199=CARTESIAN_POINT ( 'NONE',  ( -8.043339635997652337, -84.25624999999980957, 8.043339635996300530 ) ) ;
#16207=CARTESIAN_POINT ( 'NONE',  ( 18.62500000000000000, -59.34999999999983800, 1.560692158462880521E-12 ) ) ;
#16209=CARTESIAN_POINT ( 'NONE',  ( -18.62500000000000000, -34.37499999999990052, -1.562973063126292757E-12 ) ) ;
#16211=CARTESIAN_POINT ( 'NONE',  ( -18.62499999999934985, -90.53437499999978400, -7.714727599200458918 ) ) ;
#16232=CARTESIAN_POINT ( 'NONE',  ( 1.561832610794586740E-12, -28.06249999999995381, -18.62500000000000000 ) ) ;
#16243=CARTESIAN_POINT ( 'NONE',  ( 4.711679271994909435, -36.42187499999990763, -11.37499999999960387 ) ) ;
#16250=CARTESIAN_POINT ( 'NONE',  ( 5.127128379249549894, -7.251940901129065153E-16, -15.62300691738110636 ) ) ;
#16274=CARTESIAN_POINT ( 'NONE',  ( 13.16986379959834075, -14.56874999999996589, 13.16986379960055231 ) ) ;
#16282=CARTESIAN_POINT ( 'NONE',  ( 17.21696878885094861, -99.99999999999994316, 6.677246014329758950 ) ) ;
#16284=CARTESIAN_POINT ( 'NONE',  ( -8.043339635996302306, -56.19374999999985931, -8.043339635997654113 ) ) ;
#16286=CARTESIAN_POINT ( 'NONE',  ( 15.00000000000000000, -100.0000000000000000, 0.000000000000000000 ) ) ;
#16294=CARTESIAN_POINT ( 'NONE',  ( -18.62500000000064659, -33.26562499999994316, 7.714727599197333419 ) ) ;
#16300=CARTESIAN_POINT ( 'NONE',  ( -18.62500000000064659, -68.71562499999981810, 7.714727599197333419 ) ) ;
#16302=CARTESIAN_POINT ( 'NONE',  ( 7.714727599200456254, -45.82187499999987779, -18.62499999999935341 ) ) ;
#16308=VERTEX_POINT ( 'NONE', #10705 ) ;
#16326=CARTESIAN_POINT ( 'NONE',  ( -13.16986379959834252, -13.49374999999998792, -13.16986379960055409 ) ) ;
#16339=CARTESIAN_POINT ( 'NONE',  ( 3.073853547173910350, -1.028534069218512171E-14, -14.38353912379420230 ) ) ;
#16356=CARTESIAN_POINT ( 'NONE',  ( -11.37499999999960387, -7.284374999999982059, -4.711679271994911211 ) ) ;
#16373=CARTESIAN_POINT ( 'NONE',  ( 8.825897884691713102, -99.99999999999998579, 14.84509086929686283 ) ) ;
#16375=CARTESIAN_POINT ( 'NONE',  ( -11.37500000000000000, -91.57499999999977547, -9.545674412382054647E-13 ) ) ;
#16386=CARTESIAN_POINT ( 'NONE',  ( -7.714727599200466912, -35.34687499999993321, 18.62499999999935341 ) ) ;
#16393=CARTESIAN_POINT ( 'NONE',  ( 7.714727599200456254, -29.17187499999991118, -18.62499999999935341 ) ) ;
#16395=CARTESIAN_POINT ( 'NONE',  ( -7.714727599197334307, -64.55312499999983800, -18.62500000000064659 ) ) ;
#16416=CARTESIAN_POINT ( 'NONE',  ( -13.16986379960055231, -10.40624999999997513, 13.16986379959834252 ) ) ;
#16418=CARTESIAN_POINT ( 'NONE',  ( -18.62499999999935341, -47.83437499999990195, -7.714727599200458030 ) ) ;
#16432=CARTESIAN_POINT ( 'NONE',  ( 3.144316449151975501, -1.028534069218507438E-14, -14.16943933260104949 ) ) ;
#16447=CARTESIAN_POINT ( 'NONE',  ( -4.711679271993003404, -55.15312499999986784, -11.37500000000039435 ) ) ;
#16455=CARTESIAN_POINT ( 'NONE',  ( -13.16986379960055231, -10.40624999999997513, 13.16986379959834252 ) ) ;
#16461=CARTESIAN_POINT ( 'NONE',  ( 15.00000000000000000, 0.000000000000000000, 1.256933281983527907E-12 ) ) ;
#16465=CARTESIAN_POINT ( 'NONE',  ( 8.043339635997654113, -68.68124999999983515, -8.043339635996304082 ) ) ;
#16474=CARTESIAN_POINT ( 'NONE',  ( -7.714727599200466912, -68.64687499999988063, 18.62499999999935341 ) ) ;
#16482=CARTESIAN_POINT ( 'NONE',  ( -18.62500000000000000, -51.02499999999986358, -1.562973063126292757E-12 ) ) ;
#16496=( BOUNDED_SURFACE ( )  B_SPLINE_SURFACE ( 3, 2, ( 
 ( #11940, #13510, #14913, #13598, #6729, #12025, #3888, #8147, #9563, #5233, #10618, #14656, #6644, #4151, #10874, #9631, #2806, #14740, #1149, #13262, #5403, #8238, #12107, #1494, #16071, #4061, #1402, #13425, #2544, #10787, #7972, #6818, #13341, #17404, #5319, #3977, #16153, #12195, #10703, #9389, #14824, #2629, #88, #8061, #1314, #14450, #7588, #15598, #15773, #7938, #11648, #5110, #4841, #3683, #938, #3591, #17111, #3856, #10415, #10245, #3506, #17285, #850, #14533, #2337, #8919, #3772, #10330, #14278, #6261, #14622, #1201, #9003, #10502, #2164, #12968, #10588, #4929, #9185, #6349, #7851, #13310, #13056, #13226, #2418, #15684, #5198, #11565, #14360, #1115, #6529, #9097, #2508, #1028, #16939, #11907, #7770 ),
 ( #11733, #17025, #15950, #2249, #7677, #6439, #9270, #5016, #13141, #11822, #17202, #15865, #16034, #12075, #17374, #4295, #9708, #15052, #1456, #3942, #4118, #9532, #5550, #4029, #8293, #12161, #5639, #2595, #17454, #6875, #16118, #9443, #11021, #14791, #5368, #16393, #1368, #2683, #2861, #10754, #8114, #8024, #14876, #13480, #13392, #6783, #1281, #1544, #6695, #4207, #13565, #52, #5288, #10670, #14971, #2951, #8380, #2772, #5457, #10840, #9620, #13735, #9357, #14706, #16207, #8203, #6612, #6963, #12249, #233, #144, #11992, #10933, #16300, #13649, #12341, #8951, #4874, #15458, #3369, #10277, #630, #6129, #12653, #14309, #12742, #8783, #12571, #5867, #14139, #16625, #4528, #7183, #10191, #14053, #458, #9935 ),
 ( #15544, #11246, #3456, #15284, #799, #5952, #15628, #2108, #11508, #8871, #16710, #3185, #4615, #14224, #3536, #7270, #2027, #7452, #8693, #8607, #3276, #12915, #11424, #16884, #13959, #1856, #543, #7535, #12832, #11332, #719, #1940, #4790, #10022, #6209, #11595, #15370, #16972, #7363, #6041, #16796, #4702, #10107, #972, #6385, #15984, #3887, #11858, #5232, #5143, #13001, #11939, #11768, #883, #9040, #5318, #9388, #17144, #1148, #6295, #10365, #1231, #13087, #17320, #9132, #9304, #16070, #3714, #14655, #10617, #5053, #13340, #3976, #10451, #2543, #7971, #6472, #10702, #9219, #2196, #6643, #10535, #6559, #15810, #12024, #7803, #17403, #15719, #14481, #2454, #2370, #13174, #7624, #1060, #17233, #11681, #15898 ),
 ( #3806, #3623, #14570, #7709, #14393, #7884, #2282, #17057, #13261, #4962, #4484, #10873, #8060, #1313, #5908, #12699, #16751, #412, #87, #10786, #12611, #7314, #12106, #13424, #6728, #13509, #14004, #15326, #16579, #8650, #3047, #2628, #14739, #4393, #13917, #16243, #16152, #4659, #586, #5402, #6817, #11379, #12194, #11287, #8477, #14956, #7225, #1811, #4060, #1401, #9803, #9476, #15241, #14823, #502, #5492, #9893, #13828, #5820, #2717, #8146, #1728, #15149, #7142, #8564, #12528, #11204, #3139, #16665, #4572, #5997, #9979, #3230, #1897, #15764, #16842, #3412, #11466, #840, #15500, #8994, #11551, #2240, #17193, #4920, #3496, #14351, #8737, #6086, #2068, #7579, #3674, #8825, #762, #14096, #7759, #674 ),
 ( #14183, #9088, #10407, #11637, #14441, #15589, #15416, #10066, #16927, #7668, #6170, #4745, #11816, #13133, #10150, #7492, #6432, #12873, #6339, #8911, #3323, #13047, #929, #1981, #4830, #10234, #7406, #10318, #12788, #11725, #14267, #17016, #2155, #12957, #6251, #15673, #3580, #17101, #5008, #2329, #1021, #9351, #11986, #14616, #10664, #14869, #3935, #15858, #3765, #10835, #11901, #8108, #8019, #9177, #14786, #3848, #14525, #17278, #8196, #12243, #2500, #4023, #2412, #13218, #4111, #15941, #2676, #17367, #1359, #1449, #6607, #6774, #13473, #9264, #16199, #6868, #7930, #12155, #45, #14700, #13559, #12070, #5103, #5450, #13387, #9437, #13303, #9525, #16029, #2763, #1105, #1195, #5362, #5281, #2588, #10495, #1276 ),
 ( #6688, #7845, #17447, #6521, #10748, #10580, #5192, #16112, #16649, #227, #13644, #15227, #7127, #13730, #10926, #4202, #8550, #15312, #1882, #3032, #2945, #1538, #3124, #9962, #14963, #16294, #9612, #16386, #4557, #487, #1716, #11273, #5719, #5542, #136, #7046, #16566, #1627, #6956, #7298, #3215, #8287, #9701, #13987, #15048, #13902, #11101, #2853, #9876, #4472, #12333, #4290, #12425, #5632, #399, #11014, #1798, #8374, #12515, #16474, #8463, #311, #4380, #9788, #15135, #13815, #11190, #5805, #7210, #12596, #5893, #8636, #4989, #11533, #5980, #11362, #910, #1966, #15654, #15569, #16737, #4902, #11449, #4643, #7391, #15745, #2309, #4730, #11621, #10049, #3306, #11707, #6066, #10301, #2054, #8978, #9068 ),
 ( #16823, #6321, #14421, #15484, #3564, #14334, #16911, #3656, #2135, #12683, #13028, #3480, #16996, #10131, #2223, #747, #17084, #8719, #3395, #12939, #8808, #14165, #10391, #7477, #12857, #573, #6156, #4814, #7652, #10216, #8894, #15399, #14249, #14079, #12768, #657, #7561, #823, #6234, #14599, #4000, #4086, #9246, #9416, #5342, #11884, #1336, #9502, #10563, #17427, #10727, #11967, #10813, #14681, #14849, #8085, #10644, #6666, #5171, #14764, #13287, #6752, #3743, #1087, #7998, #17259, #15923, #12132, #3831, #6501, #21, #2479, #7912, #2656, #1175, #6586, #9159, #16008, #13201, #13450, #1000, #5424, #7829, #14506, #16092, #2568, #17347, #6413, #11796, #16176, #7737, #13113, #3914, #5258, #2394, #17173, #5083 ) ),
 .UNSPECIFIED., .T., .F., .F. ) 
 B_SPLINE_SURFACE_WITH_KNOTS ( ( 4, 3, 4 ),
 ( 3, 2, 2, 2, 2, 2, 2, 2, 2, 2, 2, 2, 2, 2, 2, 2, 2, 2, 2, 2, 2, 2, 2, 2, 2, 2, 2, 2, 2, 2, 2, 2, 2, 2, 2, 2, 2, 2, 2, 2, 2, 2, 2, 2, 2, 2, 2, 2, 3 ),
 ( 0.000000000000000000, 0.5000000000000000000, 1.000000000000000000 ),
 ( 0.000000000000000000, 0.02083333333333333218, 0.04166666666666666435, 0.06250000000000000000, 0.08333333333333332871, 0.1041666666666666713, 0.1250000000000000000, 0.1458333333333333426, 0.1666666666666666574, 0.1875000000000000000, 0.2083333333333333426, 0.2291666666666666574, 0.2500000000000000000, 0.2708333333333333148, 0.2916666666666666852, 0.3125000000000000000, 0.3333333333333333148, 0.3541666666666666852, 0.3750000000000000000, 0.3958333333333333148, 0.4166666666666666852, 0.4375000000000000000, 0.4583333333333333148, 0.4791666666666666852, 0.5000000000000000000, 0.5208333333333333703, 0.5416666666666666297, 0.5625000000000000000, 0.5833333333333333703, 0.6041666666666666297, 0.6250000000000000000, 0.6458333333333333703, 0.6666666666666666297, 0.6875000000000000000, 0.7083333333333333703, 0.7291666666666666297, 0.7500000000000000000, 0.7708333333333333703, 0.7916666666666666297, 0.8125000000000000000, 0.8333333333333333703, 0.8541666666666666297, 0.8750000000000000000, 0.8958333333333333703, 0.9166666666666666297, 0.9375000000000000000, 0.9583333333333333703, 0.9791666666666666297, 1.000000000000000000 ),
 .UNSPECIFIED. ) 
 GEOMETRIC_REPRESENTATION_ITEM ( )  RATIONAL_B_SPLINE_SURFACE ( (
 ( 1.000000000000000000, 0.9238795325112867385, 1.000000000000000000, 0.9238795325112867385, 1.000000000000000000, 0.9238795325112867385, 1.000000000000000000, 0.9238795325112867385, 1.000000000000000000, 0.9238795325112867385, 1.000000000000000000, 0.9238795325112867385, 1.000000000000000000, 0.9238795325112867385, 1.000000000000000000, 0.9238795325112867385, 1.000000000000000000, 0.9238795325112867385, 1.000000000000000000, 0.9238795325112867385, 1.000000000000000000, 0.9238795325112867385, 1.000000000000000000, 0.9238795325112867385, 1.000000000000000000, 0.9238795325112867385, 1.000000000000000000, 0.9238795325112867385, 1.000000000000000000, 0.9238795325112867385, 1.000000000000000000, 0.9238795325112867385, 1.000000000000000000, 0.9238795325112867385, 1.000000000000000000, 0.9238795325112867385, 1.000000000000000000, 0.9238795325112867385, 1.000000000000000000, 0.9238795325112867385, 1.000000000000000000, 0.9238795325112867385, 1.000000000000000000, 0.9238795325112867385, 1.000000000000000000, 0.9238795325112867385, 1.000000000000000000, 0.9238795325112867385, 1.000000000000000000, 0.9238795325112867385, 1.000000000000000000, 0.9238795325112867385, 1.000000000000000000, 0.9238795325112867385, 1.000000000000000000, 0.9238795325112867385, 1.000000000000000000, 0.9238795325112867385, 1.000000000000000000, 0.9238795325112867385, 1.000000000000000000, 0.9238795325112867385, 1.000000000000000000, 0.9238795325112867385, 1.000000000000000000, 0.9238795325112867385, 1.000000000000000000, 0.9238795325112867385, 1.000000000000000000, 0.9238795325112867385, 1.000000000000000000, 0.9238795325112867385, 1.000000000000000000, 0.9238795325112867385, 1.000000000000000000, 0.9238795325112867385, 1.000000000000000000, 0.9238795325112867385, 1.000000000000000000, 0.9238795325112867385, 1.000000000000000000, 0.9238795325112867385, 1.000000000000000000, 0.9238795325112867385, 1.000000000000000000, 0.9238795325112867385, 1.000000000000000000, 0.9238795325112867385, 1.000000000000000000, 0.9238795325112867385, 1.000000000000000000, 0.9238795325112867385, 1.000000000000000000, 0.9238795325112867385, 1.000000000000000000, 0.9238795325112867385, 1.000000000000000000),
 ( 0.3333333333333333703, 0.3079598441704289313, 0.3333333333333333703, 0.3079598441704289313, 0.3333333333333333703, 0.3079598441704289313, 0.3333333333333333703, 0.3079598441704289313, 0.3333333333333333703, 0.3079598441704289313, 0.3333333333333333703, 0.3079598441704289313, 0.3333333333333333703, 0.3079598441704289313, 0.3333333333333333703, 0.3079598441704289313, 0.3333333333333333703, 0.3079598441704289313, 0.3333333333333333703, 0.3079598441704289313, 0.3333333333333333703, 0.3079598441704289313, 0.3333333333333333703, 0.3079598441704289313, 0.3333333333333333703, 0.3079598441704289313, 0.3333333333333333703, 0.3079598441704289313, 0.3333333333333333703, 0.3079598441704289313, 0.3333333333333333703, 0.3079598441704289313, 0.3333333333333333703, 0.3079598441704289313, 0.3333333333333333703, 0.3079598441704289313, 0.3333333333333333703, 0.3079598441704289313, 0.3333333333333333703, 0.3079598441704289313, 0.3333333333333333703, 0.3079598441704289313, 0.3333333333333333703, 0.3079598441704289313, 0.3333333333333333703, 0.3079598441704289313, 0.3333333333333333703, 0.3079598441704289313, 0.3333333333333333703, 0.3079598441704289313, 0.3333333333333333703, 0.3079598441704289313, 0.3333333333333333703, 0.3079598441704289313, 0.3333333333333333703, 0.3079598441704289313, 0.3333333333333333703, 0.3079598441704289313, 0.3333333333333333703, 0.3079598441704289313, 0.3333333333333333703, 0.3079598441704289313, 0.3333333333333333703, 0.3079598441704289313, 0.3333333333333333703, 0.3079598441704289313, 0.3333333333333333703, 0.3079598441704289313, 0.3333333333333333703, 0.3079598441704289313, 0.3333333333333333703, 0.3079598441704289313, 0.3333333333333333703, 0.3079598441704289313, 0.3333333333333333703, 0.3079598441704289313, 0.3333333333333333703, 0.3079598441704289313, 0.3333333333333333703, 0.3079598441704289313, 0.3333333333333333703, 0.3079598441704289313, 0.3333333333333333703, 0.3079598441704289313, 0.3333333333333333703, 0.3079598441704289313, 0.3333333333333333703, 0.3079598441704289313, 0.3333333333333333703, 0.3079598441704289313, 0.3333333333333333703, 0.3079598441704289313, 0.3333333333333333703, 0.3079598441704289313, 0.3333333333333333703, 0.3079598441704289313, 0.3333333333333333703),
 ( 0.3333333333333333703, 0.3079598441704289313, 0.3333333333333333703, 0.3079598441704289313, 0.3333333333333333703, 0.3079598441704289313, 0.3333333333333333703, 0.3079598441704289313, 0.3333333333333333703, 0.3079598441704289313, 0.3333333333333333703, 0.3079598441704289313, 0.3333333333333333703, 0.3079598441704289313, 0.3333333333333333703, 0.3079598441704289313, 0.3333333333333333703, 0.3079598441704289313, 0.3333333333333333703, 0.3079598441704289313, 0.3333333333333333703, 0.3079598441704289313, 0.3333333333333333703, 0.3079598441704289313, 0.3333333333333333703, 0.3079598441704289313, 0.3333333333333333703, 0.3079598441704289313, 0.3333333333333333703, 0.3079598441704289313, 0.3333333333333333703, 0.3079598441704289313, 0.3333333333333333703, 0.3079598441704289313, 0.3333333333333333703, 0.3079598441704289313, 0.3333333333333333703, 0.3079598441704289313, 0.3333333333333333703, 0.3079598441704289313, 0.3333333333333333703, 0.3079598441704289313, 0.3333333333333333703, 0.3079598441704289313, 0.3333333333333333703, 0.3079598441704289313, 0.3333333333333333703, 0.3079598441704289313, 0.3333333333333333703, 0.3079598441704289313, 0.3333333333333333703, 0.3079598441704289313, 0.3333333333333333703, 0.3079598441704289313, 0.3333333333333333703, 0.3079598441704289313, 0.3333333333333333703, 0.3079598441704289313, 0.3333333333333333703, 0.3079598441704289313, 0.3333333333333333703, 0.3079598441704289313, 0.3333333333333333703, 0.3079598441704289313, 0.3333333333333333703, 0.3079598441704289313, 0.3333333333333333703, 0.3079598441704289313, 0.3333333333333333703, 0.3079598441704289313, 0.3333333333333333703, 0.3079598441704289313, 0.3333333333333333703, 0.3079598441704289313, 0.3333333333333333703, 0.3079598441704289313, 0.3333333333333333703, 0.3079598441704289313, 0.3333333333333333703, 0.3079598441704289313, 0.3333333333333333703, 0.3079598441704289313, 0.3333333333333333703, 0.3079598441704289313, 0.3333333333333333703, 0.3079598441704289313, 0.3333333333333333703, 0.3079598441704289313, 0.3333333333333333703, 0.3079598441704289313, 0.3333333333333333703, 0.3079598441704289313, 0.3333333333333333703, 0.3079598441704289313, 0.3333333333333333703, 0.3079598441704289313, 0.3333333333333333703),
 ( 1.000000000000000000, 0.9238795325112867385, 1.000000000000000000, 0.9238795325112867385, 1.000000000000000000, 0.9238795325112867385, 1.000000000000000000, 0.9238795325112867385, 1.000000000000000000, 0.9238795325112867385, 1.000000000000000000, 0.9238795325112867385, 1.000000000000000000, 0.9238795325112867385, 1.000000000000000000, 0.9238795325112867385, 1.000000000000000000, 0.9238795325112867385, 1.000000000000000000, 0.9238795325112867385, 1.000000000000000000, 0.9238795325112867385, 1.000000000000000000, 0.9238795325112867385, 1.000000000000000000, 0.9238795325112867385, 1.000000000000000000, 0.9238795325112867385, 1.000000000000000000, 0.9238795325112867385, 1.000000000000000000, 0.9238795325112867385, 1.000000000000000000, 0.9238795325112867385, 1.000000000000000000, 0.9238795325112867385, 1.000000000000000000, 0.9238795325112867385, 1.000000000000000000, 0.9238795325112867385, 1.000000000000000000, 0.9238795325112867385, 1.000000000000000000, 0.9238795325112867385, 1.000000000000000000, 0.9238795325112867385, 1.000000000000000000, 0.9238795325112867385, 1.000000000000000000, 0.9238795325112867385, 1.000000000000000000, 0.9238795325112867385, 1.000000000000000000, 0.9238795325112867385, 1.000000000000000000, 0.9238795325112867385, 1.000000000000000000, 0.9238795325112867385, 1.000000000000000000, 0.9238795325112867385, 1.000000000000000000, 0.9238795325112867385, 1.000000000000000000, 0.9238795325112867385, 1.000000000000000000, 0.9238795325112867385, 1.000000000000000000, 0.9238795325112867385, 1.000000000000000000, 0.9238795325112867385, 1.000000000000000000, 0.9238795325112867385, 1.000000000000000000, 0.9238795325112867385, 1.000000000000000000, 0.9238795325112867385, 1.000000000000000000, 0.9238795325112867385, 1.000000000000000000, 0.9238795325112867385, 1.000000000000000000, 0.9238795325112867385, 1.000000000000000000, 0.9238795325112867385, 1.000000000000000000, 0.9238795325112867385, 1.000000000000000000, 0.9238795325112867385, 1.000000000000000000, 0.9238795325112867385, 1.000000000000000000, 0.9238795325112867385, 1.000000000000000000, 0.9238795325112867385, 1.000000000000000000, 0.9238795325112867385, 1.000000000000000000),
 ( 0.3333333333333333703, 0.3079598441704289313, 0.3333333333333333703, 0.3079598441704289313, 0.3333333333333333703, 0.3079598441704289313, 0.3333333333333333703, 0.3079598441704289313, 0.3333333333333333703, 0.3079598441704289313, 0.3333333333333333703, 0.3079598441704289313, 0.3333333333333333703, 0.3079598441704289313, 0.3333333333333333703, 0.3079598441704289313, 0.3333333333333333703, 0.3079598441704289313, 0.3333333333333333703, 0.3079598441704289313, 0.3333333333333333703, 0.3079598441704289313, 0.3333333333333333703, 0.3079598441704289313, 0.3333333333333333703, 0.3079598441704289313, 0.3333333333333333703, 0.3079598441704289313, 0.3333333333333333703, 0.3079598441704289313, 0.3333333333333333703, 0.3079598441704289313, 0.3333333333333333703, 0.3079598441704289313, 0.3333333333333333703, 0.3079598441704289313, 0.3333333333333333703, 0.3079598441704289313, 0.3333333333333333703, 0.3079598441704289313, 0.3333333333333333703, 0.3079598441704289313, 0.3333333333333333703, 0.3079598441704289313, 0.3333333333333333703, 0.3079598441704289313, 0.3333333333333333703, 0.3079598441704289313, 0.3333333333333333703, 0.3079598441704289313, 0.3333333333333333703, 0.3079598441704289313, 0.3333333333333333703, 0.3079598441704289313, 0.3333333333333333703, 0.3079598441704289313, 0.3333333333333333703, 0.3079598441704289313, 0.3333333333333333703, 0.3079598441704289313, 0.3333333333333333703, 0.3079598441704289313, 0.3333333333333333703, 0.3079598441704289313, 0.3333333333333333703, 0.3079598441704289313, 0.3333333333333333703, 0.3079598441704289313, 0.3333333333333333703, 0.3079598441704289313, 0.3333333333333333703, 0.3079598441704289313, 0.3333333333333333703, 0.3079598441704289313, 0.3333333333333333703, 0.3079598441704289313, 0.3333333333333333703, 0.3079598441704289313, 0.3333333333333333703, 0.3079598441704289313, 0.3333333333333333703, 0.3079598441704289313, 0.3333333333333333703, 0.3079598441704289313, 0.3333333333333333703, 0.3079598441704289313, 0.3333333333333333703, 0.3079598441704289313, 0.3333333333333333703, 0.3079598441704289313, 0.3333333333333333703, 0.3079598441704289313, 0.3333333333333333703, 0.3079598441704289313, 0.3333333333333333703, 0.3079598441704289313, 0.3333333333333333703),
 ( 0.3333333333333333703, 0.3079598441704289313, 0.3333333333333333703, 0.3079598441704289313, 0.3333333333333333703, 0.3079598441704289313, 0.3333333333333333703, 0.3079598441704289313, 0.3333333333333333703, 0.3079598441704289313, 0.3333333333333333703, 0.3079598441704289313, 0.3333333333333333703, 0.3079598441704289313, 0.3333333333333333703, 0.3079598441704289313, 0.3333333333333333703, 0.3079598441704289313, 0.3333333333333333703, 0.3079598441704289313, 0.3333333333333333703, 0.3079598441704289313, 0.3333333333333333703, 0.3079598441704289313, 0.3333333333333333703, 0.3079598441704289313, 0.3333333333333333703, 0.3079598441704289313, 0.3333333333333333703, 0.3079598441704289313, 0.3333333333333333703, 0.3079598441704289313, 0.3333333333333333703, 0.3079598441704289313, 0.3333333333333333703, 0.3079598441704289313, 0.3333333333333333703, 0.3079598441704289313, 0.3333333333333333703, 0.3079598441704289313, 0.3333333333333333703, 0.3079598441704289313, 0.3333333333333333703, 0.3079598441704289313, 0.3333333333333333703, 0.3079598441704289313, 0.3333333333333333703, 0.3079598441704289313, 0.3333333333333333703, 0.3079598441704289313, 0.3333333333333333703, 0.3079598441704289313, 0.3333333333333333703, 0.3079598441704289313, 0.3333333333333333703, 0.3079598441704289313, 0.3333333333333333703, 0.3079598441704289313, 0.3333333333333333703, 0.3079598441704289313, 0.3333333333333333703, 0.3079598441704289313, 0.3333333333333333703, 0.3079598441704289313, 0.3333333333333333703, 0.3079598441704289313, 0.3333333333333333703, 0.3079598441704289313, 0.3333333333333333703, 0.3079598441704289313, 0.3333333333333333703, 0.3079598441704289313, 0.3333333333333333703, 0.3079598441704289313, 0.3333333333333333703, 0.3079598441704289313, 0.3333333333333333703, 0.3079598441704289313, 0.3333333333333333703, 0.3079598441704289313, 0.3333333333333333703, 0.3079598441704289313, 0.3333333333333333703, 0.3079598441704289313, 0.3333333333333333703, 0.3079598441704289313, 0.3333333333333333703, 0.3079598441704289313, 0.3333333333333333703, 0.3079598441704289313, 0.3333333333333333703, 0.3079598441704289313, 0.3333333333333333703, 0.3079598441704289313, 0.3333333333333333703, 0.3079598441704289313, 0.3333333333333333703),
 ( 1.000000000000000000, 0.9238795325112867385, 1.000000000000000000, 0.9238795325112867385, 1.000000000000000000, 0.9238795325112867385, 1.000000000000000000, 0.9238795325112867385, 1.000000000000000000, 0.9238795325112867385, 1.000000000000000000, 0.9238795325112867385, 1.000000000000000000, 0.9238795325112867385, 1.000000000000000000, 0.9238795325112867385, 1.000000000000000000, 0.9238795325112867385, 1.000000000000000000, 0.9238795325112867385, 1.000000000000000000, 0.9238795325112867385, 1.000000000000000000, 0.9238795325112867385, 1.000000000000000000, 0.9238795325112867385, 1.000000000000000000, 0.9238795325112867385, 1.000000000000000000, 0.9238795325112867385, 1.000000000000000000, 0.9238795325112867385, 1.000000000000000000, 0.9238795325112867385, 1.000000000000000000, 0.9238795325112867385, 1.000000000000000000, 0.9238795325112867385, 1.000000000000000000, 0.9238795325112867385, 1.000000000000000000, 0.9238795325112867385, 1.000000000000000000, 0.9238795325112867385, 1.000000000000000000, 0.9238795325112867385, 1.000000000000000000, 0.9238795325112867385, 1.000000000000000000, 0.9238795325112867385, 1.000000000000000000, 0.9238795325112867385, 1.000000000000000000, 0.9238795325112867385, 1.000000000000000000, 0.9238795325112867385, 1.000000000000000000, 0.9238795325112867385, 1.000000000000000000, 0.9238795325112867385, 1.000000000000000000, 0.9238795325112867385, 1.000000000000000000, 0.9238795325112867385, 1.000000000000000000, 0.9238795325112867385, 1.000000000000000000, 0.9238795325112867385, 1.000000000000000000, 0.9238795325112867385, 1.000000000000000000, 0.9238795325112867385, 1.000000000000000000, 0.9238795325112867385, 1.000000000000000000, 0.9238795325112867385, 1.000000000000000000, 0.9238795325112867385, 1.000000000000000000, 0.9238795325112867385, 1.000000000000000000, 0.9238795325112867385, 1.000000000000000000, 0.9238795325112867385, 1.000000000000000000, 0.9238795325112867385, 1.000000000000000000, 0.9238795325112867385, 1.000000000000000000, 0.9238795325112867385, 1.000000000000000000, 0.9238795325112867385, 1.000000000000000000, 0.9238795325112867385, 1.000000000000000000, 0.9238795325112867385, 1.000000000000000000) ) ) 
 REPRESENTATION_ITEM ( '' )  SURFACE ( )  );
#16507=CARTESIAN_POINT ( 'NONE',  ( -1.564113515457998370E-12, -86.33749999999982094, 18.62500000000000000 ) ) ;
#16520=CARTESIAN_POINT ( 'NONE',  ( 3.329803442097187371, -7.135244913870566388E-13, -15.09609079982930524 ) ) ;
#16536=CARTESIAN_POINT ( 'NONE',  ( -8.043339635996302306, -22.89374999999994387, -8.043339635997654113 ) ) ;
#16542=CIRCLE ( 'NONE', #11195, 3.624999999999999556 ) ;
#16555=CARTESIAN_POINT ( 'NONE',  ( 11.37499999999960210, -98.85937499999975842, 4.711679271994918317 ) ) ;
#16556=AXIS2_PLACEMENT_3D ( 'NONE', #14609, #17094, #9169 ) ;
#16566=CARTESIAN_POINT ( 'NONE',  ( 1.561832610794586740E-12, -44.71249999999991331, -18.62500000000000000 ) ) ;
#16574=CARTESIAN_POINT ( 'NONE',  ( -7.714727599200466912, -70.79687499999981526, 18.62499999999935341 ) ) ;
#16579=CARTESIAN_POINT ( 'NONE',  ( -9.552639591052204498E-13, -29.13749999999993179, 11.37500000000000000 ) ) ;
#16595=CARTESIAN_POINT ( 'NONE',  ( -7.714727599197334307, -95.70312499999980105, -18.62500000000064659 ) ) ;
#16608=CARTESIAN_POINT ( 'NONE',  ( 11.21760822425125603, -2.318222727469663182E-13, -13.78532672430268491 ) ) ;
#16625=CARTESIAN_POINT ( 'NONE',  ( -13.16986379960055409, -86.40624999999977263, 13.16986379959834252 ) ) ;
#16626=CARTESIAN_POINT ( 'NONE',  ( 4.711679271993006068, -80.12812499999981242, 11.37500000000039257 ) ) ;
#16649=CARTESIAN_POINT ( 'NONE',  ( -18.62500000000000000, -15.57499999999998153, -1.562973063126292757E-12 ) ) ;
#16654=AXIS2_PLACEMENT_3D ( 'NONE', #186, #4335, #13945 ) ;
#16657=CARTESIAN_POINT ( 'NONE',  ( -1.564113515457998370E-12, -55.18749999999985079, 18.62500000000000000 ) ) ;
#16665=CARTESIAN_POINT ( 'NONE',  ( 9.538709233711902776E-13, -70.76249999999983231, -11.37500000000000000 ) ) ;
#16680=CARTESIAN_POINT ( 'NONE',  ( 7.714727599200458030, -3.121874999999992628, -18.62499999999934985 ) ) ;
#16682=CARTESIAN_POINT ( 'NONE',  ( 18.62500000000064659, -58.24062499999988063, -7.714727599197336083 ) ) ;
#16710=CARTESIAN_POINT ( 'NONE',  ( -8.043339635997654113, -3.156249999999973355, 8.043339635996304082 ) ) ;
#16711=CARTESIAN_POINT ( 'NONE',  ( 11.37500000000039435, -84.29062499999980673, -4.711679271993003404 ) ) ;
#16716=CARTESIAN_POINT ( 'NONE',  ( 18.62499999999934985, -32.25937499999992042, 7.714727599200467800 ) ) ;
#16737=CARTESIAN_POINT ( 'NONE',  ( 18.62500000000000000, -90.49999999999980105, 1.560692158462880521E-12 ) ) ;
#16743=CARTESIAN_POINT ( 'NONE',  ( 11.37500000000000178, -26.04999999999992255, 9.531744055041752924E-13 ) ) ;
#16751=CARTESIAN_POINT ( 'NONE',  ( 11.37500000000000000, -16.64999999999995950, 9.531744055041752924E-13 ) ) ;
#16767=CARTESIAN_POINT ( 'NONE',  ( -18.62500000000000000, -8.324999999999979750, -1.562973063126292555E-12 ) ) ;
#16769=CARTESIAN_POINT ( 'NONE',  ( 13.16986379960055054, -2.081249999999994937, -13.16986379959834430 ) ) ;
#16796=CARTESIAN_POINT ( 'NONE',  ( -11.37500000000000178, -34.37499999999990052, -9.545674412382054647E-13 ) ) ;
#16797=CARTESIAN_POINT ( 'NONE',  ( 11.37499999999960210, -32.25937499999992042, 4.711679271994917428 ) ) ;
#16800=CARTESIAN_POINT ( 'NONE',  ( -13.16986379959834252, -72.84374999999981526, -13.16986379960055054 ) ) ;
#16823=CARTESIAN_POINT ( 'NONE',  ( 18.62500000000000000, 0.000000000000000000, 1.560692158462880521E-12 ) ) ;
#16833=CARTESIAN_POINT ( 'NONE',  ( 4.711679271993006957, -39.57812499999989342, 11.37500000000039613 ) ) ;
#16842=CARTESIAN_POINT ( 'NONE',  ( -4.711679271994916540, -78.04687499999982947, 11.37499999999960210 ) ) ;
#16857=CARTESIAN_POINT ( 'NONE',  ( 18.62499999999934630, -48.90937499999989058, 7.714727599200467800 ) ) ;
#16859=CARTESIAN_POINT ( 'NONE',  ( 7.714727599197338748, -46.82812499999989342, 18.62500000000063949 ) ) ;
#16870=( NAMED_UNIT ( * ) SI_UNIT ( $, .STERADIAN. ) SOLID_ANGLE_UNIT ( ) );
#16875=CARTESIAN_POINT ( 'NONE',  ( 11.37499999999960210, -82.20937499999980957, 4.711679271994918317 ) ) ;
#16884=CARTESIAN_POINT ( 'NONE',  ( -11.37499999999960743, -16.68437499999993889, -4.711679271994912099 ) ) ;
#16890=CARTESIAN_POINT ( 'NONE',  ( 7.714727599200458030, -69.72187499999984084, -18.62499999999935341 ) ) ;
#16898=( NAMED_UNIT ( * ) SI_UNIT ( $, .STERADIAN. ) SOLID_ANGLE_UNIT ( ) );
#16906=ORIENTED_EDGE ( 'NONE', *, *, #4067, .T. ) ;
#16911=CARTESIAN_POINT ( 'NONE',  ( -13.16986379959834252, -6.243749999999985256, -13.16986379960055054 ) ) ;
#16921=CARTESIAN_POINT ( 'NONE',  ( -8.043339635997654113, -3.156249999999973355, 8.043339635996304082 ) ) ;
#16927=CARTESIAN_POINT ( 'NONE',  ( -11.37499999999999645, -15.57499999999997975, -9.545674412382054647E-13 ) ) ;
#16939=CARTESIAN_POINT ( 'NONE',  ( 13.16986379959834075, -97.81874999999976694, 13.16986379960055231 ) ) ;
#16941=CARTESIAN_POINT ( 'NONE',  ( 13.16986379959834075, -47.86874999999988489, 13.16986379960055231 ) ) ;
#16943=CARTESIAN_POINT ( 'NONE',  ( 18.62500000000064304, -17.69062499999995453, -7.714727599197335195 ) ) ;
#16959=( BOUNDED_CURVE ( )  B_SPLINE_CURVE ( 2, ( #5421, #1332, #16173, #2915, #12214, #9326, #2564, #16356, #6748, #199, #1512, #10809, #6927, #4082, #7994, #12305, #13701, #1251, #5604, #8345, #12395, #4703, #16536, #3277, #12572, #1941, #2028, #7184, #7364, #8694, #9850, #16797, #7453, #8523, #15371, #14054, #9936, #8784, #12654, #12833, #6042, #4350, #459, #11333, #14140, #5868, #5694, #631, #1685, #15197, #544, #12743, #9759, #16447, #15104, #7271, #11425, #3003, #11161, #8433, #3370, #13960, #4443, #7101, #13873, #371, #10108, #12485, #15459, #5953, #1775, #13787, #5776, #11074, #3097, #11247, #8608, #16626, #4529, #15285, #3186, #16711, #1857, #4616, #10023, #3624, #5144, #7710, #973, #6210, #4963, #11769, #800, #15629, #6473, #16973, #3457 ),
 .UNSPECIFIED., .F., .F. ) 
 B_SPLINE_CURVE_WITH_KNOTS ( ( 3, 2, 2, 2, 2, 2, 2, 2, 2, 2, 2, 2, 2, 2, 2, 2, 2, 2, 2, 2, 2, 2, 2, 2, 2, 2, 2, 2, 2, 2, 2, 2, 2, 2, 2, 2, 2, 2, 2, 2, 2, 2, 2, 2, 2, 2, 2, 2, 3 ),
 ( 0.000000000000000000, 0.02083333333333333218, 0.04166666666666666435, 0.06250000000000000000, 0.08333333333333332871, 0.1041666666666666713, 0.1250000000000000000, 0.1458333333333333426, 0.1666666666666666574, 0.1875000000000000000, 0.2083333333333333426, 0.2291666666666666574, 0.2500000000000000000, 0.2708333333333333148, 0.2916666666666666852, 0.3125000000000000000, 0.3333333333333333148, 0.3541666666666666852, 0.3750000000000000000, 0.3958333333333333148, 0.4166666666666666852, 0.4375000000000000000, 0.4583333333333333148, 0.4791666666666666852, 0.5000000000000000000, 0.5208333333333333703, 0.5416666666666666297, 0.5625000000000000000, 0.5833333333333333703, 0.6041666666666666297, 0.6250000000000000000, 0.6458333333333333703, 0.6666666666666666297, 0.6875000000000000000, 0.7083333333333333703, 0.7291666666666666297, 0.7500000000000000000, 0.7708333333333333703, 0.7916666666666666297, 0.8125000000000000000, 0.8333333333333333703, 0.8541666666666666297, 0.8750000000000000000, 0.8958333333333333703, 0.9166666666666666297, 0.9375000000000000000, 0.9583333333333333703, 0.9791666666666666297, 1.000000000000000000 ),
 .UNSPECIFIED. ) 
 CURVE ( )  GEOMETRIC_REPRESENTATION_ITEM ( )  RATIONAL_B_SPLINE_CURVE ( ( 1.000000000000000000, 0.9238795325112867385, 1.000000000000000000, 0.9238795325112867385, 1.000000000000000000, 0.9238795325112867385, 1.000000000000000000, 0.9238795325112867385, 1.000000000000000000, 0.9238795325112867385, 1.000000000000000000, 0.9238795325112867385, 1.000000000000000000, 0.9238795325112867385, 1.000000000000000000, 0.9238795325112867385, 1.000000000000000000, 0.9238795325112867385, 1.000000000000000000, 0.9238795325112867385, 1.000000000000000000, 0.9238795325112867385, 1.000000000000000000, 0.9238795325112867385, 1.000000000000000000, 0.9238795325112867385, 1.000000000000000000, 0.9238795325112867385, 1.000000000000000000, 0.9238795325112867385, 1.000000000000000000, 0.9238795325112867385, 1.000000000000000000, 0.9238795325112867385, 1.000000000000000000, 0.9238795325112867385, 1.000000000000000000, 0.9238795325112867385, 1.000000000000000000, 0.9238795325112867385, 1.000000000000000000, 0.9238795325112867385, 1.000000000000000000, 0.9238795325112867385, 1.000000000000000000, 0.9238795325112867385, 1.000000000000000000, 0.9238795325112867385, 1.000000000000000000, 0.9238795325112867385, 1.000000000000000000, 0.9238795325112867385, 1.000000000000000000, 0.9238795325112867385, 1.000000000000000000, 0.9238795325112867385, 1.000000000000000000, 0.9238795325112867385, 1.000000000000000000, 0.9238795325112867385, 1.000000000000000000, 0.9238795325112867385, 1.000000000000000000, 0.9238795325112867385, 1.000000000000000000, 0.9238795325112867385, 1.000000000000000000, 0.9238795325112867385, 1.000000000000000000, 0.9238795325112867385, 1.000000000000000000, 0.9238795325112867385, 1.000000000000000000, 0.9238795325112867385, 1.000000000000000000, 0.9238795325112867385, 1.000000000000000000, 0.9238795325112867385, 1.000000000000000000, 0.9238795325112867385, 1.000000000000000000, 0.9238795325112867385, 1.000000000000000000, 0.9238795325112867385, 1.000000000000000000, 0.9238795325112867385, 1.000000000000000000, 0.9238795325112867385, 1.000000000000000000, 0.9238795325112867385, 1.000000000000000000, 0.9238795325112867385, 1.000000000000000000, 0.9238795325112867385, 1.000000000000000000, 0.9238795325112867385, 1.000000000000000000 ) ) 
 REPRESENTATION_ITEM ( '' )  );
#16962=CARTESIAN_POINT ( 'NONE',  ( 4.711679271993006957, -20.77812499999997087, 11.37500000000039257 ) ) ;
#16972=CARTESIAN_POINT ( 'NONE',  ( -4.711679271993003404, -31.25312499999991545, -11.37500000000039613 ) ) ;
#16973=CARTESIAN_POINT ( 'NONE',  ( 11.37499999999960210, -98.85937499999975842, 4.711679271994917428 ) ) ;
#16977=CARTESIAN_POINT ( 'NONE',  ( 13.16986379959834075, -31.21874999999992539, 13.16986379960055231 ) ) ;
#16996=CARTESIAN_POINT ( 'NONE',  ( -1.564113515457998572E-12, -12.48749999999997051, 18.62500000000000000 ) ) ;
#17003=CARTESIAN_POINT ( 'NONE',  ( 11.37637957285810586, -100.0000000000000000, 0.000000000000000000 ) ) ;
#17005=CARTESIAN_POINT ( 'NONE',  ( -4.711679271994916540, -54.14687499999985931, 11.37499999999960565 ) ) ;
#17016=CARTESIAN_POINT ( 'NONE',  ( 11.37499999999960210, -39.50937499999993463, 4.711679271994916540 ) ) ;
#17021=DIRECTION ( 'NONE',  ( 0.000000000000000000, -0.000000000000000000, 1.000000000000000000 ) ) ;
#17025=CARTESIAN_POINT ( 'NONE',  ( 18.62500000000064659, 6.209375000000004974, -7.714727599197336083 ) ) ;
#17027=CARTESIAN_POINT ( 'NONE',  ( 13.16986379960055054, -68.68124999999983515, -13.16986379959834430 ) ) ;
#17029=CARTESIAN_POINT ( 'NONE',  ( 1.561832610794586538E-12, -54.11249999999986926, -18.62500000000000000 ) ) ;
#17047=CARTESIAN_POINT ( 'NONE',  ( -11.37500000000039613, -66.56562499999985505, 4.711679271993000739 ) ) ;
#17057=CARTESIAN_POINT ( 'NONE',  ( -11.37499999999960387, -7.284374999999982059, -4.711679271994910323 ) ) ;
#17061=CARTESIAN_POINT ( 'NONE',  ( 18.62499999999934985, -48.90937499999988347, 7.714727599200467800 ) ) ;
#17082=EDGE_LOOP ( 'NONE', ( #3392, #3824, #14093, #5081 ) ) ;
#17084=CARTESIAN_POINT ( 'NONE',  ( 18.62500000000000000, -16.64999999999995950, 1.560692158462880521E-12 ) ) ;
#17093=CARTESIAN_POINT ( 'NONE',  ( -11.37500000000039790, -2.115624999999976996, 4.711679271993001628 ) ) ;
#17094=DIRECTION ( 'NONE',  ( 0.000000000000000000, 0.000000000000000000, 1.000000000000000000 ) ) ;
#17101=CARTESIAN_POINT ( 'NONE',  ( -4.711679271993001628, -45.75312499999991189, -11.37500000000039613 ) ) ;
#17111=CARTESIAN_POINT ( 'NONE',  ( -18.62500000000000000, -58.27499999999986358, -1.562973063126292555E-12 ) ) ;
#17113=CARTESIAN_POINT ( 'NONE',  ( 18.62499999999934630, -65.55937499999984652, 7.714727599200467800 ) ) ;
#17115=CARTESIAN_POINT ( 'NONE',  ( -1.564113515457998572E-12, -45.78749999999988773, 18.62500000000000000 ) ) ;
#17125=DIRECTION ( 'NONE',  ( 0.000000000000000000, -0.000000000000000000, 1.000000000000000000 ) ) ;
#17134=CARTESIAN_POINT ( 'NONE',  ( 4.711679271994911211, -76.97187499999985505, -11.37499999999960210 ) ) ;
#17138=APPLICATION_CONTEXT ( 'automotive_design' ) ;
#17144=CARTESIAN_POINT ( 'NONE',  ( -11.37500000000039790, -52.06562499999986926, 4.711679271993001628 ) ) ;
#17148=CARTESIAN_POINT ( 'NONE',  ( -1.564113515457998572E-12, -95.73749999999976978, 18.62500000000000000 ) ) ;
#17173=CARTESIAN_POINT ( 'NONE',  ( 18.62499999999934630, -98.85937499999975842, 7.714727599200467800 ) ) ;
#17183=CARTESIAN_POINT ( 'NONE',  ( -11.37499999999960743, -83.28437499999976978, -4.711679271994912099 ) ) ;
#17193=CARTESIAN_POINT ( 'NONE',  ( 4.711679271994909435, -86.37187499999978968, -11.37499999999960387 ) ) ;
#17202=CARTESIAN_POINT ( 'NONE',  ( -13.16986379960055409, -3.156249999999973355, 13.16986379959834252 ) ) ;
#17204=CARTESIAN_POINT ( 'NONE',  ( 7.714727599200456254, -12.52187499999995524, -18.62499999999935341 ) ) ;
#17206=CARTESIAN_POINT ( 'NONE',  ( 7.714727599200458030, -69.72187499999982663, -18.62499999999934985 ) ) ;
#17223=CARTESIAN_POINT ( 'NONE',  ( 11.37499999999999645, -73.84999999999983800, 9.531744055041752924E-13 ) ) ;
#17231=EDGE_LOOP ( 'NONE', ( #5357, #2584, #17315, #12678 ) ) ;
#17233=CARTESIAN_POINT ( 'NONE',  ( 8.043339635996302306, -90.56874999999976694, 8.043339635997654113 ) ) ;
#17259=CARTESIAN_POINT ( 'NONE',  ( 18.62500000000064304, -67.64062499999984368, -7.714727599197335195 ) ) ;
#17266=CARTESIAN_POINT ( 'NONE',  ( 4.722607142260388358, -99.99999999999995737, 12.69610481275498870 ) ) ;
#17268=CARTESIAN_POINT ( 'NONE',  ( -4.711679271994916540, -28.09687499999992966, 11.37499999999960210 ) ) ;
#17276=AXIS2_PLACEMENT_3D ( 'NONE', #32, #1010, #6421 ) ;
#17278=CARTESIAN_POINT ( 'NONE',  ( -11.37500000000039613, -66.56562499999985505, 4.711679271993000739 ) ) ;
#17285=CARTESIAN_POINT ( 'NONE',  ( 7.714727599197338748, -63.47812499999984226, 18.62500000000063949 ) ) ;
#17288=CARTESIAN_POINT ( 'NONE',  ( -18.62500000000000000, -91.57499999999977547, -1.562973063126292555E-12 ) ) ;
#17290=CARTESIAN_POINT ( 'NONE',  ( -18.62500000000000000, -74.92499999999982663, -1.562973063126292555E-12 ) ) ;
#17309=CARTESIAN_POINT ( 'NONE',  ( -8.043339635996300530, -30.14374999999994742, -8.043339635997652337 ) ) ;
#17315=ORIENTED_EDGE ( 'NONE', *, *, #12372, .T. ) ;
#17320=CARTESIAN_POINT ( 'NONE',  ( 11.37499999999960565, -58.30937499999983231, 4.711679271994918317 ) ) ;
#17347=CARTESIAN_POINT ( 'NONE',  ( -13.16986379959834252, -89.49374999999979252, -13.16986379960055054 ) ) ;
#17355=EDGE_CURVE ( 'NONE', #7272, #7126, #15232, .T. ) ;
#17356=CARTESIAN_POINT ( 'NONE',  ( 11.14820950268467392, -99.99999999999997158, 13.72570587197042791 ) ) ;
#17358=CARTESIAN_POINT ( 'NONE',  ( 4.711679271993006957, -89.52812499999977547, 11.37500000000039613 ) ) ;
#17367=CARTESIAN_POINT ( 'NONE',  ( 4.711679271994911211, -76.97187499999985505, -11.37499999999960210 ) ) ;
#17374=CARTESIAN_POINT ( 'NONE',  ( 13.16986379959833897, -7.318749999999964118, 13.16986379960055409 ) ) ;
#17376=CARTESIAN_POINT ( 'NONE',  ( 13.16986379959834075, -97.81874999999976694, 13.16986379960055231 ) ) ;
#17395=CARTESIAN_POINT ( 'NONE',  ( -11.37499999999999645, -82.17499999999982663, -9.545674412382054647E-13 ) ) ;
#17403=CARTESIAN_POINT ( 'NONE',  ( -8.043339635996304082, -82.24374999999977831, -8.043339635997652337 ) ) ;
#17404=CARTESIAN_POINT ( 'NONE',  ( 18.62500000000064304, -34.34062499999991047, -7.714727599197335195 ) ) ;
#17427=CARTESIAN_POINT ( 'NONE',  ( 18.62500000000064304, -50.99062499999987352, -7.714727599197335195 ) ) ;
#17437=CARTESIAN_POINT ( 'NONE',  ( 9.226448456246030716, -99.99999999999998579, 14.69264636604441776 ) ) ;
#17439=CARTESIAN_POINT ( 'NONE',  ( 11.37499999999960565, -74.95937499999980957, 4.711679271994918317 ) ) ;
#17447=CARTESIAN_POINT ( 'NONE',  ( 13.16986379960055409, -9.331249999999993605, -13.16986379959834430 ) ) ;
#17454=CARTESIAN_POINT ( 'NONE',  ( -1.564113515457998370E-12, -21.88749999999992824, 18.62500000000000000 ) ) ;
#17456=CARTESIAN_POINT ( 'NONE',  ( -18.62499999999934985, -90.53437499999978400, -7.714727599200458918 ) ) ;
#17460=CARTESIAN_POINT ( 'NONE',  ( -7.714727599197335195, -71.80312499999982379, -18.62500000000064304 ) ) ;
#17479=CARTESIAN_POINT ( 'NONE',  ( -18.62500000000064659, -33.26562499999994316, 7.714727599197333419 ) ) ;
#17513=COLOUR_RGB('Grey',0.48,0.52,0.57);
#17514=FILL_AREA_STYLE_COLOUR('',#17513);
#17515=FILL_AREA_STYLE('',(#17514));
#17516=SURFACE_STYLE_FILL_AREA(#17515);
#17517=SURFACE_SIDE_STYLE('',(#17516));
#17518=SURFACE_STYLE_USAGE(.BOTH.,#17517);
#17519=PRESENTATION_STYLE_ASSIGNMENT((#17518));
ENDSEC;
END-ISO-10303-21;
